ISO-10303-21;
HEADER;
/* Generated by software containing ST-Developer
 * from STEP Tools, Inc. (www.steptools.com) 
 */

FILE_DESCRIPTION(
/* description */ (''),
/* implementation_level */ '2;1');

FILE_NAME(
/* name */ 'LINEAR GUIDE(Mirror).step',
/* time_stamp */ '2026-10-19T01:17:59+06:00',
/* author */ (''),
/* organization */ (''),
/* preprocessor_version */ 'ST-DEVELOPER v20.2',
/* originating_system */ 'Autodesk Translation Framework v15.15.0.0',
/* authorisation */ '');

FILE_SCHEMA (('AUTOMOTIVE_DESIGN { 1 0 10303 214 3 1 1 }'));
ENDSEC;

DATA;
#10=MECHANICAL_DESIGN_GEOMETRIC_PRESENTATION_REPRESENTATION('',(#729,#730,#731),#48369);
#613=SHAPE_REPRESENTATION_RELATIONSHIP('SRR','None',#48413,#624);
#624=ADVANCED_BREP_SHAPE_REPRESENTATION('',(#755,#756,#757),#48358);
#635=FACE_BOUND('',#2301,.T.);
#636=FACE_BOUND('',#2302,.T.);
#637=FACE_BOUND('',#2310,.T.);
#638=FACE_BOUND('',#2311,.T.);
#639=FACE_BOUND('',#2320,.T.);
#640=FACE_BOUND('',#2321,.T.);
#641=FACE_BOUND('',#2331,.T.);
#642=FACE_BOUND('',#2332,.T.);
#729=STYLED_ITEM('',(#48510),#755);
#730=STYLED_ITEM('',(#48510),#756);
#731=STYLED_ITEM('',(#48510),#757);
#755=MANIFOLD_SOLID_BREP('Body1',#20108);
#756=MANIFOLD_SOLID_BREP('Body2',#20109);
#757=MANIFOLD_SOLID_BREP('Body3',#20110);
#781=CYLINDRICAL_SURFACE('',#20276,0.45000000000016);
#782=CYLINDRICAL_SURFACE('',#20278,2.46743797397104);
#783=CYLINDRICAL_SURFACE('',#20280,0.724999999999998);
#784=CYLINDRICAL_SURFACE('',#20283,0.59999999999997);
#785=CYLINDRICAL_SURFACE('',#20285,2.36402292474775);
#786=CYLINDRICAL_SURFACE('',#20287,1.39999999999995);
#787=CYLINDRICAL_SURFACE('',#20290,1.04999999999995);
#788=CYLINDRICAL_SURFACE('',#20293,1.04999999999981);
#789=CYLINDRICAL_SURFACE('',#20303,1.04999999999996);
#790=CYLINDRICAL_SURFACE('',#20311,0.450000000000123);
#791=CYLINDRICAL_SURFACE('',#20313,2.46743797397101);
#792=CYLINDRICAL_SURFACE('',#20315,0.72500000000001);
#793=CYLINDRICAL_SURFACE('',#20318,0.599999999999987);
#794=CYLINDRICAL_SURFACE('',#20320,2.3640229247478);
#795=CYLINDRICAL_SURFACE('',#20322,1.39999999999978);
#796=CYLINDRICAL_SURFACE('',#20325,1.05);
#797=CYLINDRICAL_SURFACE('',#20329,0.45000000000016);
#798=CYLINDRICAL_SURFACE('',#20332,2.46743797397104);
#799=CYLINDRICAL_SURFACE('',#20335,0.724999999999998);
#800=CYLINDRICAL_SURFACE('',#20339,0.59999999999997);
#801=CYLINDRICAL_SURFACE('',#20342,2.36402292474775);
#802=CYLINDRICAL_SURFACE('',#20365,2.16656587073651);
#803=CYLINDRICAL_SURFACE('',#20387,2.16656587073651);
#804=CYLINDRICAL_SURFACE('',#20388,3.00000000000001);
#805=CYLINDRICAL_SURFACE('',#20390,3.00000000000001);
#806=CYLINDRICAL_SURFACE('',#20392,3.00000000000001);
#807=CYLINDRICAL_SURFACE('',#20394,3.00000000000001);
#808=CYLINDRICAL_SURFACE('',#20400,1.04999999999981);
#809=CYLINDRICAL_SURFACE('',#20402,1.04999999999995);
#810=CYLINDRICAL_SURFACE('',#20404,1.39999999999995);
#811=CYLINDRICAL_SURFACE('',#20409,1.04999999999996);
#812=CYLINDRICAL_SURFACE('',#20411,1.05);
#813=CYLINDRICAL_SURFACE('',#20413,1.39999999999978);
#814=CYLINDRICAL_SURFACE('',#20414,2.3640229247478);
#815=CYLINDRICAL_SURFACE('',#20415,0.599999999999987);
#816=CYLINDRICAL_SURFACE('',#20417,0.72500000000001);
#817=CYLINDRICAL_SURFACE('',#20418,2.46743797397101);
#818=CYLINDRICAL_SURFACE('',#20419,0.450000000000123);
#819=CYLINDRICAL_SURFACE('',#20422,1.39999999999995);
#820=CYLINDRICAL_SURFACE('',#20426,1.04999999999995);
#821=CYLINDRICAL_SURFACE('',#20430,1.04999999999981);
#822=CYLINDRICAL_SURFACE('',#20443,1.04999999999996);
#823=CYLINDRICAL_SURFACE('',#20461,1.05);
#824=CYLINDRICAL_SURFACE('',#20464,1.39999999999978);
#825=CYLINDRICAL_SURFACE('',#20466,2.3640229247478);
#826=CYLINDRICAL_SURFACE('',#20468,0.599999999999987);
#827=CYLINDRICAL_SURFACE('',#20471,0.72500000000001);
#828=CYLINDRICAL_SURFACE('',#20473,2.46743797397101);
#829=CYLINDRICAL_SURFACE('',#20475,0.450000000000123);
#830=CYLINDRICAL_SURFACE('',#20480,0.45000000000016);
#831=CYLINDRICAL_SURFACE('',#20482,2.46743797397104);
#832=CYLINDRICAL_SURFACE('',#20484,0.724999999999998);
#833=CYLINDRICAL_SURFACE('',#20487,0.59999999999997);
#834=CYLINDRICAL_SURFACE('',#20489,2.36402292474775);
#1207=FACE_OUTER_BOUND('',#2251,.T.);
#1208=FACE_OUTER_BOUND('',#2252,.T.);
#1209=FACE_OUTER_BOUND('',#2253,.T.);
#1210=FACE_OUTER_BOUND('',#2254,.T.);
#1211=FACE_OUTER_BOUND('',#2255,.T.);
#1212=FACE_OUTER_BOUND('',#2256,.T.);
#1213=FACE_OUTER_BOUND('',#2257,.T.);
#1214=FACE_OUTER_BOUND('',#2258,.T.);
#1215=FACE_OUTER_BOUND('',#2259,.T.);
#1216=FACE_OUTER_BOUND('',#2260,.T.);
#1217=FACE_OUTER_BOUND('',#2261,.T.);
#1218=FACE_OUTER_BOUND('',#2262,.T.);
#1219=FACE_OUTER_BOUND('',#2263,.T.);
#1220=FACE_OUTER_BOUND('',#2264,.T.);
#1221=FACE_OUTER_BOUND('',#2265,.T.);
#1222=FACE_OUTER_BOUND('',#2266,.T.);
#1223=FACE_OUTER_BOUND('',#2267,.T.);
#1224=FACE_OUTER_BOUND('',#2268,.T.);
#1225=FACE_OUTER_BOUND('',#2269,.T.);
#1226=FACE_OUTER_BOUND('',#2270,.T.);
#1227=FACE_OUTER_BOUND('',#2271,.T.);
#1228=FACE_OUTER_BOUND('',#2272,.T.);
#1229=FACE_OUTER_BOUND('',#2273,.T.);
#1230=FACE_OUTER_BOUND('',#2274,.T.);
#1231=FACE_OUTER_BOUND('',#2275,.T.);
#1232=FACE_OUTER_BOUND('',#2276,.T.);
#1233=FACE_OUTER_BOUND('',#2277,.T.);
#1234=FACE_OUTER_BOUND('',#2278,.T.);
#1235=FACE_OUTER_BOUND('',#2279,.T.);
#1236=FACE_OUTER_BOUND('',#2280,.T.);
#1237=FACE_OUTER_BOUND('',#2281,.T.);
#1238=FACE_OUTER_BOUND('',#2282,.T.);
#1239=FACE_OUTER_BOUND('',#2283,.T.);
#1240=FACE_OUTER_BOUND('',#2284,.T.);
#1241=FACE_OUTER_BOUND('',#2285,.T.);
#1242=FACE_OUTER_BOUND('',#2286,.T.);
#1243=FACE_OUTER_BOUND('',#2287,.T.);
#1244=FACE_OUTER_BOUND('',#2288,.T.);
#1245=FACE_OUTER_BOUND('',#2289,.T.);
#1246=FACE_OUTER_BOUND('',#2290,.T.);
#1247=FACE_OUTER_BOUND('',#2291,.T.);
#1248=FACE_OUTER_BOUND('',#2292,.T.);
#1249=FACE_OUTER_BOUND('',#2293,.T.);
#1250=FACE_OUTER_BOUND('',#2294,.T.);
#1251=FACE_OUTER_BOUND('',#2295,.T.);
#1252=FACE_OUTER_BOUND('',#2296,.T.);
#1253=FACE_OUTER_BOUND('',#2297,.T.);
#1254=FACE_OUTER_BOUND('',#2298,.T.);
#1255=FACE_OUTER_BOUND('',#2299,.T.);
#1256=FACE_OUTER_BOUND('',#2300,.T.);
#1257=FACE_OUTER_BOUND('',#2303,.T.);
#1258=FACE_OUTER_BOUND('',#2304,.T.);
#1259=FACE_OUTER_BOUND('',#2305,.T.);
#1260=FACE_OUTER_BOUND('',#2306,.T.);
#1261=FACE_OUTER_BOUND('',#2307,.T.);
#1262=FACE_OUTER_BOUND('',#2308,.T.);
#1263=FACE_OUTER_BOUND('',#2309,.T.);
#1264=FACE_OUTER_BOUND('',#2312,.T.);
#1265=FACE_OUTER_BOUND('',#2313,.T.);
#1266=FACE_OUTER_BOUND('',#2314,.T.);
#1267=FACE_OUTER_BOUND('',#2315,.T.);
#1268=FACE_OUTER_BOUND('',#2316,.T.);
#1269=FACE_OUTER_BOUND('',#2317,.T.);
#1270=FACE_OUTER_BOUND('',#2318,.T.);
#1271=FACE_OUTER_BOUND('',#2319,.T.);
#1272=FACE_OUTER_BOUND('',#2322,.T.);
#1273=FACE_OUTER_BOUND('',#2323,.T.);
#1274=FACE_OUTER_BOUND('',#2324,.T.);
#1275=FACE_OUTER_BOUND('',#2325,.T.);
#1276=FACE_OUTER_BOUND('',#2326,.T.);
#1277=FACE_OUTER_BOUND('',#2327,.T.);
#1278=FACE_OUTER_BOUND('',#2328,.T.);
#1279=FACE_OUTER_BOUND('',#2329,.T.);
#1280=FACE_OUTER_BOUND('',#2330,.T.);
#1281=FACE_OUTER_BOUND('',#2333,.T.);
#1282=FACE_OUTER_BOUND('',#2334,.T.);
#1283=FACE_OUTER_BOUND('',#2335,.T.);
#1284=FACE_OUTER_BOUND('',#2336,.T.);
#1285=FACE_OUTER_BOUND('',#2337,.T.);
#1286=FACE_OUTER_BOUND('',#2338,.T.);
#1287=FACE_OUTER_BOUND('',#2339,.T.);
#1288=FACE_OUTER_BOUND('',#2340,.T.);
#1289=FACE_OUTER_BOUND('',#2341,.T.);
#1290=FACE_OUTER_BOUND('',#2342,.T.);
#1291=FACE_OUTER_BOUND('',#2343,.T.);
#1292=FACE_OUTER_BOUND('',#2344,.T.);
#1293=FACE_OUTER_BOUND('',#2345,.T.);
#1294=FACE_OUTER_BOUND('',#2346,.T.);
#1295=FACE_OUTER_BOUND('',#2347,.T.);
#1296=FACE_OUTER_BOUND('',#2348,.T.);
#1297=FACE_OUTER_BOUND('',#2349,.T.);
#1298=FACE_OUTER_BOUND('',#2350,.T.);
#1299=FACE_OUTER_BOUND('',#2351,.T.);
#1300=FACE_OUTER_BOUND('',#2352,.T.);
#1301=FACE_OUTER_BOUND('',#2353,.T.);
#1302=FACE_OUTER_BOUND('',#2354,.T.);
#1303=FACE_OUTER_BOUND('',#2355,.T.);
#1304=FACE_OUTER_BOUND('',#2356,.T.);
#1305=FACE_OUTER_BOUND('',#2357,.T.);
#1306=FACE_OUTER_BOUND('',#2358,.T.);
#1307=FACE_OUTER_BOUND('',#2359,.T.);
#1308=FACE_OUTER_BOUND('',#2360,.T.);
#1309=FACE_OUTER_BOUND('',#2361,.T.);
#1310=FACE_OUTER_BOUND('',#2362,.T.);
#1311=FACE_OUTER_BOUND('',#2363,.T.);
#1312=FACE_OUTER_BOUND('',#2364,.T.);
#1313=FACE_OUTER_BOUND('',#2365,.T.);
#1314=FACE_OUTER_BOUND('',#2366,.T.);
#1315=FACE_OUTER_BOUND('',#2367,.T.);
#1316=FACE_OUTER_BOUND('',#2368,.T.);
#1317=FACE_OUTER_BOUND('',#2369,.T.);
#1318=FACE_OUTER_BOUND('',#2370,.T.);
#1319=FACE_OUTER_BOUND('',#2371,.T.);
#1320=FACE_OUTER_BOUND('',#2372,.T.);
#1321=FACE_OUTER_BOUND('',#2373,.T.);
#1322=FACE_OUTER_BOUND('',#2374,.T.);
#1323=FACE_OUTER_BOUND('',#2375,.T.);
#1324=FACE_OUTER_BOUND('',#2376,.T.);
#1325=FACE_OUTER_BOUND('',#2377,.T.);
#1326=FACE_OUTER_BOUND('',#2378,.T.);
#1327=FACE_OUTER_BOUND('',#2379,.T.);
#1328=FACE_OUTER_BOUND('',#2380,.T.);
#1329=FACE_OUTER_BOUND('',#2381,.T.);
#1330=FACE_OUTER_BOUND('',#2382,.T.);
#1331=FACE_OUTER_BOUND('',#2383,.T.);
#1332=FACE_OUTER_BOUND('',#2384,.T.);
#2251=EDGE_LOOP('',(#12651,#12652,#12653,#12654,#12655,#12656,#12657,#12658,
#12659,#12660,#12661,#12662,#12663,#12664,#12665,#12666,#12667,#12668,#12669,
#12670,#12671,#12672,#12673,#12674,#12675,#12676,#12677,#12678,#12679,#12680,
#12681,#12682,#12683,#12684,#12685,#12686));
#2252=EDGE_LOOP('',(#12687,#12688,#12689,#12690));
#2253=EDGE_LOOP('',(#12691,#12692,#12693,#12694));
#2254=EDGE_LOOP('',(#12695,#12696,#12697,#12698));
#2255=EDGE_LOOP('',(#12699,#12700,#12701,#12702));
#2256=EDGE_LOOP('',(#12703,#12704,#12705,#12706));
#2257=EDGE_LOOP('',(#12707,#12708,#12709,#12710));
#2258=EDGE_LOOP('',(#12711,#12712,#12713,#12714));
#2259=EDGE_LOOP('',(#12715,#12716,#12717,#12718));
#2260=EDGE_LOOP('',(#12719,#12720,#12721,#12722));
#2261=EDGE_LOOP('',(#12723,#12724,#12725,#12726));
#2262=EDGE_LOOP('',(#12727,#12728,#12729,#12730));
#2263=EDGE_LOOP('',(#12731,#12732,#12733,#12734));
#2264=EDGE_LOOP('',(#12735,#12736,#12737,#12738));
#2265=EDGE_LOOP('',(#12739,#12740,#12741,#12742));
#2266=EDGE_LOOP('',(#12743,#12744,#12745,#12746));
#2267=EDGE_LOOP('',(#12747,#12748,#12749,#12750));
#2268=EDGE_LOOP('',(#12751,#12752,#12753,#12754));
#2269=EDGE_LOOP('',(#12755,#12756,#12757,#12758));
#2270=EDGE_LOOP('',(#12759,#12760,#12761,#12762));
#2271=EDGE_LOOP('',(#12763,#12764,#12765,#12766));
#2272=EDGE_LOOP('',(#12767,#12768,#12769,#12770));
#2273=EDGE_LOOP('',(#12771,#12772,#12773,#12774));
#2274=EDGE_LOOP('',(#12775,#12776,#12777,#12778));
#2275=EDGE_LOOP('',(#12779,#12780,#12781,#12782));
#2276=EDGE_LOOP('',(#12783,#12784,#12785,#12786));
#2277=EDGE_LOOP('',(#12787,#12788,#12789,#12790));
#2278=EDGE_LOOP('',(#12791,#12792,#12793,#12794));
#2279=EDGE_LOOP('',(#12795,#12796,#12797,#12798));
#2280=EDGE_LOOP('',(#12799,#12800,#12801,#12802));
#2281=EDGE_LOOP('',(#12803,#12804,#12805,#12806));
#2282=EDGE_LOOP('',(#12807,#12808,#12809,#12810));
#2283=EDGE_LOOP('',(#12811,#12812,#12813,#12814));
#2284=EDGE_LOOP('',(#12815,#12816,#12817,#12818));
#2285=EDGE_LOOP('',(#12819,#12820,#12821,#12822));
#2286=EDGE_LOOP('',(#12823,#12824,#12825,#12826));
#2287=EDGE_LOOP('',(#12827,#12828,#12829,#12830));
#2288=EDGE_LOOP('',(#12831,#12832,#12833,#12834,#12835,#12836,#12837,#12838,
#12839,#12840,#12841,#12842,#12843,#12844,#12845,#12846,#12847,#12848,#12849,
#12850,#12851,#12852,#12853,#12854,#12855,#12856,#12857,#12858,#12859,#12860,
#12861,#12862,#12863,#12864,#12865,#12866));
#2289=EDGE_LOOP('',(#12867,#12868,#12869,#12870));
#2290=EDGE_LOOP('',(#12871,#12872,#12873,#12874));
#2291=EDGE_LOOP('',(#12875,#12876,#12877,#12878));
#2292=EDGE_LOOP('',(#12879,#12880,#12881,#12882));
#2293=EDGE_LOOP('',(#12883,#12884,#12885,#12886));
#2294=EDGE_LOOP('',(#12887,#12888,#12889,#12890));
#2295=EDGE_LOOP('',(#12891,#12892,#12893,#12894));
#2296=EDGE_LOOP('',(#12895,#12896,#12897,#12898,#12899,#12900,#12901,#12902,
#12903,#12904,#12905,#12906,#12907,#12908,#12909,#12910,#12911,#12912,#12913,
#12914,#12915,#12916,#12917,#12918,#12919,#12920,#12921,#12922,#12923,#12924,
#12925,#12926,#12927,#12928,#12929,#12930,#12931,#12932,#12933,#12934,#12935,
#12936,#12937,#12938));
#2297=EDGE_LOOP('',(#12939,#12940,#12941,#12942));
#2298=EDGE_LOOP('',(#12943,#12944,#12945,#12946));
#2299=EDGE_LOOP('',(#12947,#12948,#12949,#12950));
#2300=EDGE_LOOP('',(#12951,#12952,#12953,#12954));
#2301=EDGE_LOOP('',(#12955));
#2302=EDGE_LOOP('',(#12956));
#2303=EDGE_LOOP('',(#12957,#12958,#12959,#12960));
#2304=EDGE_LOOP('',(#12961,#12962,#12963,#12964));
#2305=EDGE_LOOP('',(#12965,#12966,#12967,#12968,#12969,#12970,#12971,#12972,
#12973,#12974,#12975,#12976,#12977,#12978,#12979,#12980,#12981,#12982,#12983,
#12984,#12985,#12986,#12987,#12988,#12989,#12990,#12991,#12992,#12993,#12994,
#12995,#12996,#12997,#12998,#12999,#13000,#13001,#13002,#13003,#13004,#13005,
#13006,#13007,#13008));
#2306=EDGE_LOOP('',(#13009,#13010,#13011,#13012));
#2307=EDGE_LOOP('',(#13013,#13014,#13015,#13016));
#2308=EDGE_LOOP('',(#13017,#13018,#13019,#13020));
#2309=EDGE_LOOP('',(#13021,#13022,#13023,#13024));
#2310=EDGE_LOOP('',(#13025));
#2311=EDGE_LOOP('',(#13026));
#2312=EDGE_LOOP('',(#13027,#13028,#13029,#13030));
#2313=EDGE_LOOP('',(#13031,#13032,#13033,#13034));
#2314=EDGE_LOOP('',(#13035,#13036,#13037,#13038));
#2315=EDGE_LOOP('',(#13039,#13040,#13041,#13042));
#2316=EDGE_LOOP('',(#13043,#13044,#13045,#13046));
#2317=EDGE_LOOP('',(#13047,#13048,#13049,#13050));
#2318=EDGE_LOOP('',(#13051,#13052,#13053,#13054));
#2319=EDGE_LOOP('',(#13055,#13056,#13057,#13058));
#2320=EDGE_LOOP('',(#13059));
#2321=EDGE_LOOP('',(#13060));
#2322=EDGE_LOOP('',(#13061,#13062,#13063,#13064));
#2323=EDGE_LOOP('',(#13065,#13066,#13067,#13068));
#2324=EDGE_LOOP('',(#13069,#13070,#13071,#13072));
#2325=EDGE_LOOP('',(#13073,#13074,#13075,#13076));
#2326=EDGE_LOOP('',(#13077,#13078,#13079,#13080));
#2327=EDGE_LOOP('',(#13081,#13082,#13083,#13084));
#2328=EDGE_LOOP('',(#13085,#13086,#13087,#13088));
#2329=EDGE_LOOP('',(#13089,#13090,#13091,#13092));
#2330=EDGE_LOOP('',(#13093,#13094,#13095,#13096));
#2331=EDGE_LOOP('',(#13097));
#2332=EDGE_LOOP('',(#13098));
#2333=EDGE_LOOP('',(#13099,#13100,#13101,#13102));
#2334=EDGE_LOOP('',(#13103,#13104,#13105,#13106));
#2335=EDGE_LOOP('',(#13107,#13108,#13109,#13110));
#2336=EDGE_LOOP('',(#13111,#13112,#13113,#13114));
#2337=EDGE_LOOP('',(#13115,#13116,#13117,#13118));
#2338=EDGE_LOOP('',(#13119,#13120,#13121,#13122));
#2339=EDGE_LOOP('',(#13123,#13124,#13125,#13126));
#2340=EDGE_LOOP('',(#13127,#13128,#13129,#13130));
#2341=EDGE_LOOP('',(#13131,#13132,#13133,#13134));
#2342=EDGE_LOOP('',(#13135,#13136,#13137,#13138));
#2343=EDGE_LOOP('',(#13139,#13140,#13141,#13142));
#2344=EDGE_LOOP('',(#13143,#13144,#13145,#13146));
#2345=EDGE_LOOP('',(#13147,#13148,#13149,#13150));
#2346=EDGE_LOOP('',(#13151,#13152,#13153,#13154));
#2347=EDGE_LOOP('',(#13155,#13156,#13157,#13158));
#2348=EDGE_LOOP('',(#13159,#13160,#13161,#13162));
#2349=EDGE_LOOP('',(#13163,#13164,#13165,#13166));
#2350=EDGE_LOOP('',(#13167,#13168,#13169,#13170));
#2351=EDGE_LOOP('',(#13171,#13172,#13173,#13174));
#2352=EDGE_LOOP('',(#13175,#13176,#13177,#13178));
#2353=EDGE_LOOP('',(#13179,#13180,#13181,#13182));
#2354=EDGE_LOOP('',(#13183,#13184,#13185,#13186));
#2355=EDGE_LOOP('',(#13187,#13188,#13189,#13190));
#2356=EDGE_LOOP('',(#13191,#13192,#13193,#13194));
#2357=EDGE_LOOP('',(#13195,#13196,#13197,#13198));
#2358=EDGE_LOOP('',(#13199,#13200,#13201,#13202));
#2359=EDGE_LOOP('',(#13203,#13204,#13205,#13206));
#2360=EDGE_LOOP('',(#13207,#13208,#13209,#13210));
#2361=EDGE_LOOP('',(#13211,#13212,#13213,#13214));
#2362=EDGE_LOOP('',(#13215,#13216,#13217,#13218));
#2363=EDGE_LOOP('',(#13219,#13220,#13221,#13222,#13223,#13224,#13225,#13226,
#13227,#13228,#13229,#13230,#13231,#13232,#13233,#13234,#13235,#13236,#13237,
#13238,#13239,#13240,#13241,#13242,#13243,#13244,#13245,#13246,#13247,#13248,
#13249,#13250,#13251,#13252,#13253,#13254));
#2364=EDGE_LOOP('',(#13255,#13256,#13257,#13258));
#2365=EDGE_LOOP('',(#13259,#13260,#13261,#13262));
#2366=EDGE_LOOP('',(#13263,#13264,#13265,#13266));
#2367=EDGE_LOOP('',(#13267,#13268,#13269,#13270));
#2368=EDGE_LOOP('',(#13271,#13272,#13273,#13274));
#2369=EDGE_LOOP('',(#13275,#13276,#13277,#13278));
#2370=EDGE_LOOP('',(#13279,#13280,#13281,#13282));
#2371=EDGE_LOOP('',(#13283,#13284,#13285,#13286));
#2372=EDGE_LOOP('',(#13287,#13288,#13289,#13290));
#2373=EDGE_LOOP('',(#13291,#13292,#13293,#13294));
#2374=EDGE_LOOP('',(#13295,#13296,#13297,#13298));
#2375=EDGE_LOOP('',(#13299,#13300,#13301,#13302));
#2376=EDGE_LOOP('',(#13303,#13304,#13305,#13306));
#2377=EDGE_LOOP('',(#13307,#13308,#13309,#13310));
#2378=EDGE_LOOP('',(#13311,#13312,#13313,#13314));
#2379=EDGE_LOOP('',(#13315,#13316,#13317,#13318));
#2380=EDGE_LOOP('',(#13319,#13320,#13321,#13322));
#2381=EDGE_LOOP('',(#13323,#13324,#13325,#13326));
#2382=EDGE_LOOP('',(#13327,#13328,#13329,#13330));
#2383=EDGE_LOOP('',(#13331,#13332,#13333,#13334));
#2384=EDGE_LOOP('',(#13335,#13336,#13337,#13338,#13339,#13340,#13341,#13342,
#13343,#13344,#13345,#13346,#13347,#13348,#13349,#13350,#13351,#13352,#13353,
#13354,#13355,#13356,#13357,#13358,#13359,#13360,#13361,#13362,#13363,#13364,
#13365,#13366,#13367,#13368,#13369,#13370));
#3389=CIRCLE('',#20259,1.04999999999996);
#3390=CIRCLE('',#20260,1.05);
#3391=CIRCLE('',#20261,1.39999999999978);
#3392=CIRCLE('',#20262,2.3640229247478);
#3393=CIRCLE('',#20263,0.599999999999987);
#3394=CIRCLE('',#20264,0.72500000000001);
#3395=CIRCLE('',#20265,2.46743797397101);
#3396=CIRCLE('',#20266,0.450000000000123);
#3397=CIRCLE('',#20267,0.45000000000016);
#3398=CIRCLE('',#20268,2.46743797397104);
#3399=CIRCLE('',#20269,0.724999999999998);
#3400=CIRCLE('',#20270,0.59999999999997);
#3401=CIRCLE('',#20271,2.36402292474775);
#3402=CIRCLE('',#20272,1.39999999999995);
#3403=CIRCLE('',#20273,1.04999999999995);
#3404=CIRCLE('',#20274,1.04999999999981);
#3405=CIRCLE('',#20277,0.45000000000016);
#3406=CIRCLE('',#20279,2.46743797397104);
#3407=CIRCLE('',#20281,0.724999999999998);
#3408=CIRCLE('',#20284,0.59999999999997);
#3409=CIRCLE('',#20286,2.36402292474775);
#3410=CIRCLE('',#20288,1.39999999999995);
#3411=CIRCLE('',#20291,1.04999999999995);
#3412=CIRCLE('',#20294,1.04999999999981);
#3413=CIRCLE('',#20304,1.04999999999996);
#3414=CIRCLE('',#20312,0.450000000000123);
#3415=CIRCLE('',#20314,2.46743797397101);
#3416=CIRCLE('',#20316,0.72500000000001);
#3417=CIRCLE('',#20319,0.599999999999987);
#3418=CIRCLE('',#20321,2.3640229247478);
#3419=CIRCLE('',#20323,1.39999999999978);
#3420=CIRCLE('',#20326,1.05);
#3421=CIRCLE('',#20330,0.45000000000016);
#3422=CIRCLE('',#20331,0.45000000000016);
#3423=CIRCLE('',#20333,2.46743797397104);
#3424=CIRCLE('',#20334,2.46743797397104);
#3425=CIRCLE('',#20336,0.724999999999998);
#3426=CIRCLE('',#20337,0.724999999999998);
#3427=CIRCLE('',#20340,0.59999999999997);
#3428=CIRCLE('',#20341,0.59999999999997);
#3429=CIRCLE('',#20343,2.36402292474775);
#3430=CIRCLE('',#20344,2.36402292474775);
#3431=CIRCLE('',#20346,1.04999999999981);
#3432=CIRCLE('',#20347,1.04999999999995);
#3433=CIRCLE('',#20348,1.39999999999995);
#3434=CIRCLE('',#20349,0.450000000000123);
#3435=CIRCLE('',#20350,2.46743797397101);
#3436=CIRCLE('',#20351,0.72500000000001);
#3437=CIRCLE('',#20352,0.599999999999987);
#3438=CIRCLE('',#20353,2.3640229247478);
#3439=CIRCLE('',#20354,1.39999999999978);
#3440=CIRCLE('',#20355,1.05);
#3441=CIRCLE('',#20356,1.04999999999996);
#3442=CIRCLE('',#20357,2.16656587073651);
#3443=CIRCLE('',#20358,2.16656587073651);
#3444=CIRCLE('',#20363,3.00000000000001);
#3445=CIRCLE('',#20364,3.00000000000001);
#3446=CIRCLE('',#20366,2.16656587073651);
#3447=CIRCLE('',#20369,2.16656587073651);
#3448=CIRCLE('',#20370,1.04999999999996);
#3449=CIRCLE('',#20371,1.05);
#3450=CIRCLE('',#20372,1.39999999999978);
#3451=CIRCLE('',#20373,2.3640229247478);
#3452=CIRCLE('',#20374,0.599999999999987);
#3453=CIRCLE('',#20375,0.72500000000001);
#3454=CIRCLE('',#20376,2.46743797397101);
#3455=CIRCLE('',#20377,0.450000000000123);
#3456=CIRCLE('',#20378,1.39999999999995);
#3457=CIRCLE('',#20379,1.04999999999995);
#3458=CIRCLE('',#20380,1.04999999999981);
#3459=CIRCLE('',#20385,3.00000000000001);
#3460=CIRCLE('',#20386,3.00000000000001);
#3461=CIRCLE('',#20389,3.00000000000001);
#3462=CIRCLE('',#20391,3.00000000000001);
#3463=CIRCLE('',#20393,3.00000000000001);
#3464=CIRCLE('',#20395,3.00000000000001);
#3465=CIRCLE('',#20423,1.39999999999995);
#3466=CIRCLE('',#20424,1.39999999999995);
#3467=CIRCLE('',#20427,1.04999999999995);
#3468=CIRCLE('',#20428,1.04999999999995);
#3469=CIRCLE('',#20431,1.04999999999981);
#3470=CIRCLE('',#20432,1.04999999999981);
#3471=CIRCLE('',#20444,1.04999999999996);
#3472=CIRCLE('',#20445,1.04999999999996);
#3473=CIRCLE('',#20447,1.05);
#3474=CIRCLE('',#20448,1.39999999999978);
#3475=CIRCLE('',#20449,2.3640229247478);
#3476=CIRCLE('',#20450,0.599999999999987);
#3477=CIRCLE('',#20451,0.72500000000001);
#3478=CIRCLE('',#20452,2.46743797397101);
#3479=CIRCLE('',#20453,0.450000000000123);
#3480=CIRCLE('',#20454,0.45000000000016);
#3481=CIRCLE('',#20455,2.46743797397104);
#3482=CIRCLE('',#20456,0.724999999999998);
#3483=CIRCLE('',#20457,0.59999999999997);
#3484=CIRCLE('',#20458,2.36402292474775);
#3485=CIRCLE('',#20462,1.05);
#3486=CIRCLE('',#20465,1.39999999999978);
#3487=CIRCLE('',#20467,2.3640229247478);
#3488=CIRCLE('',#20469,0.599999999999987);
#3489=CIRCLE('',#20472,0.72500000000001);
#3490=CIRCLE('',#20474,2.46743797397101);
#3491=CIRCLE('',#20476,0.450000000000123);
#3492=CIRCLE('',#20481,0.45000000000016);
#3493=CIRCLE('',#20483,2.46743797397104);
#3494=CIRCLE('',#20485,0.724999999999998);
#3495=CIRCLE('',#20488,0.59999999999997);
#3496=CIRCLE('',#20490,2.36402292474775);
#3993=LINE('',#27152,#5874);
#3994=LINE('',#27154,#5875);
#3995=LINE('',#27156,#5876);
#3996=LINE('',#27158,#5877);
#3997=LINE('',#27162,#5878);
#3998=LINE('',#27166,#5879);
#3999=LINE('',#27174,#5880);
#4000=LINE('',#27182,#5881);
#4001=LINE('',#27184,#5882);
#4002=LINE('',#27186,#5883);
#4003=LINE('',#27194,#5884);
#4004=LINE('',#27202,#5885);
#4005=LINE('',#27206,#5886);
#4006=LINE('',#27210,#5887);
#4007=LINE('',#27212,#5888);
#4008=LINE('',#27214,#5889);
#4009=LINE('',#27216,#5890);
#4010=LINE('',#27218,#5891);
#4011=LINE('',#27220,#5892);
#4012=LINE('',#27221,#5893);
#4013=LINE('',#27224,#5894);
#4014=LINE('',#27226,#5895);
#4015=LINE('',#27227,#5896);
#4016=LINE('',#27231,#5897);
#4017=LINE('',#27235,#5898);
#4018=LINE('',#27239,#5899);
#4019=LINE('',#27242,#5900);
#4020=LINE('',#27243,#5901);
#4021=LINE('',#27247,#5902);
#4022=LINE('',#27251,#5903);
#4023=LINE('',#27255,#5904);
#4024=LINE('',#27258,#5905);
#4025=LINE('',#27259,#5906);
#4026=LINE('',#27263,#5907);
#4027=LINE('',#27266,#5908);
#4028=LINE('',#27267,#5909);
#4029=LINE('',#27271,#5910);
#4030=LINE('',#27274,#5911);
#4031=LINE('',#27275,#5912);
#4032=LINE('',#27278,#5913);
#4033=LINE('',#27279,#5914);
#4034=LINE('',#27282,#5915);
#4035=LINE('',#27283,#5916);
#4036=LINE('',#27286,#5917);
#4037=LINE('',#27287,#5918);
#4038=LINE('',#27290,#5919);
#4039=LINE('',#27292,#5920);
#4040=LINE('',#27293,#5921);
#4041=LINE('',#27296,#5922);
#4042=LINE('',#27297,#5923);
#4043=LINE('',#27300,#5924);
#4044=LINE('',#27301,#5925);
#4045=LINE('',#27304,#5926);
#4046=LINE('',#27305,#5927);
#4047=LINE('',#27309,#5928);
#4048=LINE('',#27312,#5929);
#4049=LINE('',#27313,#5930);
#4050=LINE('',#27316,#5931);
#4051=LINE('',#27317,#5932);
#4052=LINE('',#27319,#5933);
#4053=LINE('',#27322,#5934);
#4054=LINE('',#27323,#5935);
#4055=LINE('',#27326,#5936);
#4056=LINE('',#27327,#5937);
#4057=LINE('',#27330,#5938);
#4058=LINE('',#27331,#5939);
#4059=LINE('',#27334,#5940);
#4060=LINE('',#27338,#5941);
#4061=LINE('',#27342,#5942);
#4062=LINE('',#27346,#5943);
#4063=LINE('',#27347,#5944);
#4064=LINE('',#27350,#5945);
#4065=LINE('',#27354,#5946);
#4066=LINE('',#27358,#5947);
#4067=LINE('',#27362,#5948);
#4068=LINE('',#27363,#5949);
#4069=LINE('',#27370,#5950);
#4070=LINE('',#27372,#5951);
#4071=LINE('',#27374,#5952);
#4072=LINE('',#27375,#5953);
#4073=LINE('',#27380,#5954);
#4074=LINE('',#27386,#5955);
#4075=LINE('',#27392,#5956);
#4076=LINE('',#27396,#5957);
#4077=LINE('',#27398,#5958);
#4078=LINE('',#27399,#5959);
#4079=LINE('',#27404,#5960);
#4080=LINE('',#27410,#5961);
#4081=LINE('',#27415,#5962);
#4082=LINE('',#27417,#5963);
#4083=LINE('',#27419,#5964);
#4084=LINE('',#27421,#5965);
#4085=LINE('',#27423,#5966);
#4086=LINE('',#27427,#5967);
#4087=LINE('',#27431,#5968);
#4088=LINE('',#27434,#5969);
#4089=LINE('',#27436,#5970);
#4090=LINE('',#27444,#5971);
#4091=LINE('',#27452,#5972);
#4092=LINE('',#27456,#5973);
#4093=LINE('',#27460,#5974);
#4094=LINE('',#27462,#5975);
#4095=LINE('',#27464,#5976);
#4096=LINE('',#27466,#5977);
#4097=LINE('',#27468,#5978);
#4098=LINE('',#27470,#5979);
#4099=LINE('',#27472,#5980);
#4100=LINE('',#27474,#5981);
#4101=LINE('',#27478,#5982);
#4102=LINE('',#27482,#5983);
#4103=LINE('',#27484,#5984);
#4104=LINE('',#27485,#5985);
#4105=LINE('',#27488,#5986);
#4106=LINE('',#27490,#5987);
#4107=LINE('',#27491,#5988);
#4108=LINE('',#27494,#5989);
#4109=LINE('',#27495,#5990);
#4110=LINE('',#27498,#5991);
#4111=LINE('',#27499,#5992);
#4112=LINE('',#27502,#5993);
#4113=LINE('',#27503,#5994);
#4114=LINE('',#27510,#5995);
#4115=LINE('',#27514,#5996);
#4116=LINE('',#27515,#5997);
#4117=LINE('',#27520,#5998);
#4118=LINE('',#27522,#5999);
#4119=LINE('',#27524,#6000);
#4120=LINE('',#27526,#6001);
#4121=LINE('',#27528,#6002);
#4122=LINE('',#27530,#6003);
#4123=LINE('',#27532,#6004);
#4124=LINE('',#27534,#6005);
#4125=LINE('',#27538,#6006);
#4126=LINE('',#27542,#6007);
#4127=LINE('',#27550,#6008);
#4128=LINE('',#27558,#6009);
#4129=LINE('',#27559,#6010);
#4130=LINE('',#27563,#6011);
#4131=LINE('',#27567,#6012);
#4132=LINE('',#27571,#6013);
#4133=LINE('',#27573,#6014);
#4134=LINE('',#27575,#6015);
#4135=LINE('',#27576,#6016);
#4136=LINE('',#27578,#6017);
#4137=LINE('',#27579,#6018);
#4138=LINE('',#27581,#6019);
#4139=LINE('',#27583,#6020);
#4140=LINE('',#27585,#6021);
#4141=LINE('',#27593,#6022);
#4142=LINE('',#27597,#6023);
#4143=LINE('',#27601,#6024);
#4144=LINE('',#27605,#6025);
#4145=LINE('',#27608,#6026);
#4146=LINE('',#27610,#6027);
#4147=LINE('',#27612,#6028);
#4148=LINE('',#27614,#6029);
#4149=LINE('',#27616,#6030);
#4150=LINE('',#27618,#6031);
#4151=LINE('',#27620,#6032);
#4152=LINE('',#27622,#6033);
#4153=LINE('',#27625,#6034);
#4154=LINE('',#27627,#6035);
#4155=LINE('',#27629,#6036);
#4156=LINE('',#27631,#6037);
#4157=LINE('',#27633,#6038);
#4158=LINE('',#27635,#6039);
#4159=LINE('',#27637,#6040);
#4160=LINE('',#27639,#6041);
#4161=LINE('',#27641,#6042);
#4162=LINE('',#27643,#6043);
#4163=LINE('',#27645,#6044);
#4164=LINE('',#27647,#6045);
#4165=LINE('',#27649,#6046);
#4166=LINE('',#27651,#6047);
#4167=LINE('',#27653,#6048);
#4168=LINE('',#27655,#6049);
#4169=LINE('',#27662,#6050);
#4170=LINE('',#27665,#6051);
#4171=LINE('',#27668,#6052);
#4172=LINE('',#27670,#6053);
#4173=LINE('',#27671,#6054);
#4174=LINE('',#27676,#6055);
#4175=LINE('',#27680,#6056);
#4176=LINE('',#27682,#6057);
#4177=LINE('',#27683,#6058);
#4178=LINE('',#27688,#6059);
#4179=LINE('',#27692,#6060);
#4180=LINE('',#27694,#6061);
#4181=LINE('',#27695,#6062);
#4182=LINE('',#27698,#6063);
#4183=LINE('',#27700,#6064);
#4184=LINE('',#27701,#6065);
#4185=LINE('',#27704,#6066);
#4186=LINE('',#27706,#6067);
#4187=LINE('',#27707,#6068);
#4188=LINE('',#27711,#6069);
#4189=LINE('',#27713,#6070);
#4190=LINE('',#27715,#6071);
#4191=LINE('',#27716,#6072);
#4192=LINE('',#27719,#6073);
#4193=LINE('',#27721,#6074);
#4194=LINE('',#27722,#6075);
#4195=LINE('',#27725,#6076);
#4196=LINE('',#27727,#6077);
#4197=LINE('',#27728,#6078);
#4198=LINE('',#27731,#6079);
#4199=LINE('',#27733,#6080);
#4200=LINE('',#27734,#6081);
#4201=LINE('',#27737,#6082);
#4202=LINE('',#27739,#6083);
#4203=LINE('',#27740,#6084);
#4204=LINE('',#27743,#6085);
#4205=LINE('',#27745,#6086);
#4206=LINE('',#27746,#6087);
#4207=LINE('',#27749,#6088);
#4208=LINE('',#27751,#6089);
#4209=LINE('',#27752,#6090);
#4210=LINE('',#27757,#6091);
#4211=LINE('',#27764,#6092);
#4212=LINE('',#27772,#6093);
#4213=LINE('',#27780,#6094);
#4214=LINE('',#27782,#6095);
#4215=LINE('',#27784,#6096);
#4216=LINE('',#27792,#6097);
#4217=LINE('',#27796,#6098);
#4218=LINE('',#27797,#6099);
#4219=LINE('',#27799,#6100);
#4220=LINE('',#27802,#6101);
#4221=LINE('',#27803,#6102);
#4222=LINE('',#27807,#6103);
#4223=LINE('',#27810,#6104);
#4224=LINE('',#27811,#6105);
#4225=LINE('',#27815,#6106);
#4226=LINE('',#27819,#6107);
#4227=LINE('',#27823,#6108);
#4228=LINE('',#27826,#6109);
#4229=LINE('',#27827,#6110);
#4230=LINE('',#27831,#6111);
#4231=LINE('',#27835,#6112);
#4232=LINE('',#27839,#6113);
#4233=LINE('',#27842,#6114);
#4234=LINE('',#27843,#6115);
#4235=LINE('',#27846,#6116);
#4236=LINE('',#27847,#6117);
#4237=LINE('',#27850,#6118);
#4238=LINE('',#27851,#6119);
#4239=LINE('',#27855,#6120);
#4240=LINE('',#27859,#6121);
#4241=LINE('',#27863,#6122);
#4242=LINE('',#27866,#6123);
#4243=LINE('',#27867,#6124);
#4244=LINE('',#27871,#6125);
#5874=VECTOR('',#21932,10.);
#5875=VECTOR('',#21933,10.);
#5876=VECTOR('',#21934,10.);
#5877=VECTOR('',#21935,10.);
#5878=VECTOR('',#21938,10.);
#5879=VECTOR('',#21941,10.);
#5880=VECTOR('',#21948,10.);
#5881=VECTOR('',#21955,10.);
#5882=VECTOR('',#21956,10.);
#5883=VECTOR('',#21957,10.);
#5884=VECTOR('',#21964,10.);
#5885=VECTOR('',#21971,10.);
#5886=VECTOR('',#21974,10.);
#5887=VECTOR('',#21977,10.);
#5888=VECTOR('',#21978,10.);
#5889=VECTOR('',#21979,10.);
#5890=VECTOR('',#21980,10.);
#5891=VECTOR('',#21981,10.);
#5892=VECTOR('',#21982,10.);
#5893=VECTOR('',#21983,10.);
#5894=VECTOR('',#21986,10.);
#5895=VECTOR('',#21987,10.);
#5896=VECTOR('',#21988,10.);
#5897=VECTOR('',#21993,10.);
#5898=VECTOR('',#21998,10.);
#5899=VECTOR('',#22003,10.);
#5900=VECTOR('',#22006,10.);
#5901=VECTOR('',#22007,10.);
#5902=VECTOR('',#22012,10.);
#5903=VECTOR('',#22017,10.);
#5904=VECTOR('',#22022,10.);
#5905=VECTOR('',#22025,10.);
#5906=VECTOR('',#22026,10.);
#5907=VECTOR('',#22031,10.);
#5908=VECTOR('',#22034,10.);
#5909=VECTOR('',#22035,10.);
#5910=VECTOR('',#22040,10.);
#5911=VECTOR('',#22043,10.);
#5912=VECTOR('',#22044,10.);
#5913=VECTOR('',#22047,10.);
#5914=VECTOR('',#22048,10.);
#5915=VECTOR('',#22051,10.);
#5916=VECTOR('',#22052,10.);
#5917=VECTOR('',#22055,10.);
#5918=VECTOR('',#22056,10.);
#5919=VECTOR('',#22059,10.);
#5920=VECTOR('',#22060,10.);
#5921=VECTOR('',#22061,10.);
#5922=VECTOR('',#22064,10.);
#5923=VECTOR('',#22065,10.);
#5924=VECTOR('',#22068,10.);
#5925=VECTOR('',#22069,10.);
#5926=VECTOR('',#22072,10.);
#5927=VECTOR('',#22073,10.);
#5928=VECTOR('',#22078,10.);
#5929=VECTOR('',#22081,10.);
#5930=VECTOR('',#22082,10.);
#5931=VECTOR('',#22085,10.);
#5932=VECTOR('',#22086,10.);
#5933=VECTOR('',#22089,10.);
#5934=VECTOR('',#22092,10.);
#5935=VECTOR('',#22093,10.);
#5936=VECTOR('',#22096,10.);
#5937=VECTOR('',#22097,10.);
#5938=VECTOR('',#22100,10.);
#5939=VECTOR('',#22101,10.);
#5940=VECTOR('',#22104,10.);
#5941=VECTOR('',#22109,10.);
#5942=VECTOR('',#22114,10.);
#5943=VECTOR('',#22119,10.);
#5944=VECTOR('',#22120,10.);
#5945=VECTOR('',#22123,10.);
#5946=VECTOR('',#22128,10.);
#5947=VECTOR('',#22133,10.);
#5948=VECTOR('',#22138,10.);
#5949=VECTOR('',#22139,10.);
#5950=VECTOR('',#22148,10.);
#5951=VECTOR('',#22149,10.);
#5952=VECTOR('',#22150,10.);
#5953=VECTOR('',#22151,10.);
#5954=VECTOR('',#22156,10.);
#5955=VECTOR('',#22163,10.);
#5956=VECTOR('',#22170,10.);
#5957=VECTOR('',#22175,10.);
#5958=VECTOR('',#22176,10.);
#5959=VECTOR('',#22177,10.);
#5960=VECTOR('',#22182,10.);
#5961=VECTOR('',#22189,10.);
#5962=VECTOR('',#22194,10.);
#5963=VECTOR('',#22195,10.);
#5964=VECTOR('',#22196,10.);
#5965=VECTOR('',#22197,10.);
#5966=VECTOR('',#22198,10.);
#5967=VECTOR('',#22201,10.);
#5968=VECTOR('',#22204,10.);
#5969=VECTOR('',#22207,10.);
#5970=VECTOR('',#22208,10.);
#5971=VECTOR('',#22215,10.);
#5972=VECTOR('',#22222,10.);
#5973=VECTOR('',#22225,10.);
#5974=VECTOR('',#22228,10.);
#5975=VECTOR('',#22229,10.);
#5976=VECTOR('',#22230,10.);
#5977=VECTOR('',#22231,10.);
#5978=VECTOR('',#22232,10.);
#5979=VECTOR('',#22233,10.);
#5980=VECTOR('',#22234,10.);
#5981=VECTOR('',#22235,10.);
#5982=VECTOR('',#22238,10.);
#5983=VECTOR('',#22241,10.);
#5984=VECTOR('',#22242,10.);
#5985=VECTOR('',#22243,10.);
#5986=VECTOR('',#22246,10.);
#5987=VECTOR('',#22247,10.);
#5988=VECTOR('',#22248,10.);
#5989=VECTOR('',#22251,10.);
#5990=VECTOR('',#22252,10.);
#5991=VECTOR('',#22255,10.);
#5992=VECTOR('',#22256,10.);
#5993=VECTOR('',#22259,10.);
#5994=VECTOR('',#22260,10.);
#5995=VECTOR('',#22267,10.);
#5996=VECTOR('',#22272,10.);
#5997=VECTOR('',#22273,10.);
#5998=VECTOR('',#22278,10.);
#5999=VECTOR('',#22279,10.);
#6000=VECTOR('',#22280,10.);
#6001=VECTOR('',#22281,10.);
#6002=VECTOR('',#22282,10.);
#6003=VECTOR('',#22283,10.);
#6004=VECTOR('',#22284,10.);
#6005=VECTOR('',#22285,10.);
#6006=VECTOR('',#22288,10.);
#6007=VECTOR('',#22291,10.);
#6008=VECTOR('',#22298,10.);
#6009=VECTOR('',#22305,10.);
#6010=VECTOR('',#22306,10.);
#6011=VECTOR('',#22309,10.);
#6012=VECTOR('',#22312,10.);
#6013=VECTOR('',#22315,10.);
#6014=VECTOR('',#22316,10.);
#6015=VECTOR('',#22317,10.);
#6016=VECTOR('',#22318,10.);
#6017=VECTOR('',#22321,10.);
#6018=VECTOR('',#22322,10.);
#6019=VECTOR('',#22325,10.);
#6020=VECTOR('',#22328,10.);
#6021=VECTOR('',#22331,10.);
#6022=VECTOR('',#22340,3.00000000000001);
#6023=VECTOR('',#22345,3.00000000000001);
#6024=VECTOR('',#22350,3.00000000000001);
#6025=VECTOR('',#22355,3.00000000000001);
#6026=VECTOR('',#22360,10.);
#6027=VECTOR('',#22363,10.);
#6028=VECTOR('',#22366,10.);
#6029=VECTOR('',#22369,10.);
#6030=VECTOR('',#22372,10.);
#6031=VECTOR('',#22375,10.);
#6032=VECTOR('',#22378,10.);
#6033=VECTOR('',#22381,10.);
#6034=VECTOR('',#22386,10.);
#6035=VECTOR('',#22389,10.);
#6036=VECTOR('',#22392,10.);
#6037=VECTOR('',#22395,10.);
#6038=VECTOR('',#22398,10.);
#6039=VECTOR('',#22401,10.);
#6040=VECTOR('',#22404,10.);
#6041=VECTOR('',#22407,10.);
#6042=VECTOR('',#22410,10.);
#6043=VECTOR('',#22413,10.);
#6044=VECTOR('',#22416,10.);
#6045=VECTOR('',#22419,10.);
#6046=VECTOR('',#22422,10.);
#6047=VECTOR('',#22425,10.);
#6048=VECTOR('',#22428,10.);
#6049=VECTOR('',#22431,10.);
#6050=VECTOR('',#22438,10.);
#6051=VECTOR('',#22441,10.);
#6052=VECTOR('',#22444,10.);
#6053=VECTOR('',#22445,10.);
#6054=VECTOR('',#22446,10.);
#6055=VECTOR('',#22451,10.);
#6056=VECTOR('',#22456,10.);
#6057=VECTOR('',#22457,10.);
#6058=VECTOR('',#22458,10.);
#6059=VECTOR('',#22463,10.);
#6060=VECTOR('',#22468,10.);
#6061=VECTOR('',#22469,10.);
#6062=VECTOR('',#22470,10.);
#6063=VECTOR('',#22473,10.);
#6064=VECTOR('',#22474,10.);
#6065=VECTOR('',#22475,10.);
#6066=VECTOR('',#22478,10.);
#6067=VECTOR('',#22479,10.);
#6068=VECTOR('',#22480,10.);
#6069=VECTOR('',#22483,10.);
#6070=VECTOR('',#22484,10.);
#6071=VECTOR('',#22485,10.);
#6072=VECTOR('',#22486,10.);
#6073=VECTOR('',#22489,10.);
#6074=VECTOR('',#22490,10.);
#6075=VECTOR('',#22491,10.);
#6076=VECTOR('',#22494,10.);
#6077=VECTOR('',#22495,10.);
#6078=VECTOR('',#22496,10.);
#6079=VECTOR('',#22499,10.);
#6080=VECTOR('',#22500,10.);
#6081=VECTOR('',#22501,10.);
#6082=VECTOR('',#22504,10.);
#6083=VECTOR('',#22505,10.);
#6084=VECTOR('',#22506,10.);
#6085=VECTOR('',#22509,10.);
#6086=VECTOR('',#22510,10.);
#6087=VECTOR('',#22511,10.);
#6088=VECTOR('',#22514,10.);
#6089=VECTOR('',#22515,10.);
#6090=VECTOR('',#22516,10.);
#6091=VECTOR('',#22521,10.);
#6092=VECTOR('',#22528,10.);
#6093=VECTOR('',#22535,10.);
#6094=VECTOR('',#22542,10.);
#6095=VECTOR('',#22543,10.);
#6096=VECTOR('',#22544,10.);
#6097=VECTOR('',#22551,10.);
#6098=VECTOR('',#22556,10.);
#6099=VECTOR('',#22557,10.);
#6100=VECTOR('',#22560,10.);
#6101=VECTOR('',#22563,10.);
#6102=VECTOR('',#22564,10.);
#6103=VECTOR('',#22569,10.);
#6104=VECTOR('',#22572,10.);
#6105=VECTOR('',#22573,10.);
#6106=VECTOR('',#22578,10.);
#6107=VECTOR('',#22583,10.);
#6108=VECTOR('',#22588,10.);
#6109=VECTOR('',#22591,10.);
#6110=VECTOR('',#22592,10.);
#6111=VECTOR('',#22597,10.);
#6112=VECTOR('',#22602,10.);
#6113=VECTOR('',#22607,10.);
#6114=VECTOR('',#22610,10.);
#6115=VECTOR('',#22611,10.);
#6116=VECTOR('',#22614,10.);
#6117=VECTOR('',#22615,10.);
#6118=VECTOR('',#22618,10.);
#6119=VECTOR('',#22619,10.);
#6120=VECTOR('',#22624,10.);
#6121=VECTOR('',#22629,10.);
#6122=VECTOR('',#22634,10.);
#6123=VECTOR('',#22637,10.);
#6124=VECTOR('',#22638,10.);
#6125=VECTOR('',#22643,10.);
#7755=VERTEX_POINT('',#27150);
#7756=VERTEX_POINT('',#27151);
#7757=VERTEX_POINT('',#27153);
#7758=VERTEX_POINT('',#27155);
#7759=VERTEX_POINT('',#27157);
#7760=VERTEX_POINT('',#27159);
#7761=VERTEX_POINT('',#27161);
#7762=VERTEX_POINT('',#27163);
#7763=VERTEX_POINT('',#27165);
#7764=VERTEX_POINT('',#27167);
#7765=VERTEX_POINT('',#27169);
#7766=VERTEX_POINT('',#27171);
#7767=VERTEX_POINT('',#27173);
#7768=VERTEX_POINT('',#27175);
#7769=VERTEX_POINT('',#27177);
#7770=VERTEX_POINT('',#27179);
#7771=VERTEX_POINT('',#27181);
#7772=VERTEX_POINT('',#27183);
#7773=VERTEX_POINT('',#27185);
#7774=VERTEX_POINT('',#27187);
#7775=VERTEX_POINT('',#27189);
#7776=VERTEX_POINT('',#27191);
#7777=VERTEX_POINT('',#27193);
#7778=VERTEX_POINT('',#27195);
#7779=VERTEX_POINT('',#27197);
#7780=VERTEX_POINT('',#27199);
#7781=VERTEX_POINT('',#27201);
#7782=VERTEX_POINT('',#27203);
#7783=VERTEX_POINT('',#27205);
#7784=VERTEX_POINT('',#27207);
#7785=VERTEX_POINT('',#27209);
#7786=VERTEX_POINT('',#27211);
#7787=VERTEX_POINT('',#27213);
#7788=VERTEX_POINT('',#27215);
#7789=VERTEX_POINT('',#27217);
#7790=VERTEX_POINT('',#27219);
#7791=VERTEX_POINT('',#27223);
#7792=VERTEX_POINT('',#27225);
#7793=VERTEX_POINT('',#27229);
#7794=VERTEX_POINT('',#27233);
#7795=VERTEX_POINT('',#27237);
#7796=VERTEX_POINT('',#27241);
#7797=VERTEX_POINT('',#27245);
#7798=VERTEX_POINT('',#27249);
#7799=VERTEX_POINT('',#27253);
#7800=VERTEX_POINT('',#27257);
#7801=VERTEX_POINT('',#27261);
#7802=VERTEX_POINT('',#27265);
#7803=VERTEX_POINT('',#27269);
#7804=VERTEX_POINT('',#27273);
#7805=VERTEX_POINT('',#27277);
#7806=VERTEX_POINT('',#27281);
#7807=VERTEX_POINT('',#27285);
#7808=VERTEX_POINT('',#27289);
#7809=VERTEX_POINT('',#27291);
#7810=VERTEX_POINT('',#27295);
#7811=VERTEX_POINT('',#27299);
#7812=VERTEX_POINT('',#27303);
#7813=VERTEX_POINT('',#27307);
#7814=VERTEX_POINT('',#27311);
#7815=VERTEX_POINT('',#27315);
#7816=VERTEX_POINT('',#27321);
#7817=VERTEX_POINT('',#27325);
#7818=VERTEX_POINT('',#27329);
#7819=VERTEX_POINT('',#27333);
#7820=VERTEX_POINT('',#27337);
#7821=VERTEX_POINT('',#27341);
#7822=VERTEX_POINT('',#27345);
#7823=VERTEX_POINT('',#27349);
#7824=VERTEX_POINT('',#27353);
#7825=VERTEX_POINT('',#27357);
#7826=VERTEX_POINT('',#27361);
#7827=VERTEX_POINT('',#27368);
#7828=VERTEX_POINT('',#27369);
#7829=VERTEX_POINT('',#27371);
#7830=VERTEX_POINT('',#27373);
#7831=VERTEX_POINT('',#27377);
#7832=VERTEX_POINT('',#27379);
#7833=VERTEX_POINT('',#27383);
#7834=VERTEX_POINT('',#27385);
#7835=VERTEX_POINT('',#27389);
#7836=VERTEX_POINT('',#27391);
#7837=VERTEX_POINT('',#27395);
#7838=VERTEX_POINT('',#27397);
#7839=VERTEX_POINT('',#27401);
#7840=VERTEX_POINT('',#27403);
#7841=VERTEX_POINT('',#27407);
#7842=VERTEX_POINT('',#27409);
#7843=VERTEX_POINT('',#27413);
#7844=VERTEX_POINT('',#27414);
#7845=VERTEX_POINT('',#27416);
#7846=VERTEX_POINT('',#27418);
#7847=VERTEX_POINT('',#27420);
#7848=VERTEX_POINT('',#27422);
#7849=VERTEX_POINT('',#27424);
#7850=VERTEX_POINT('',#27426);
#7851=VERTEX_POINT('',#27428);
#7852=VERTEX_POINT('',#27430);
#7853=VERTEX_POINT('',#27433);
#7854=VERTEX_POINT('',#27435);
#7855=VERTEX_POINT('',#27437);
#7856=VERTEX_POINT('',#27439);
#7857=VERTEX_POINT('',#27441);
#7858=VERTEX_POINT('',#27443);
#7859=VERTEX_POINT('',#27445);
#7860=VERTEX_POINT('',#27447);
#7861=VERTEX_POINT('',#27449);
#7862=VERTEX_POINT('',#27451);
#7863=VERTEX_POINT('',#27453);
#7864=VERTEX_POINT('',#27455);
#7865=VERTEX_POINT('',#27457);
#7866=VERTEX_POINT('',#27459);
#7867=VERTEX_POINT('',#27461);
#7868=VERTEX_POINT('',#27463);
#7869=VERTEX_POINT('',#27465);
#7870=VERTEX_POINT('',#27467);
#7871=VERTEX_POINT('',#27469);
#7872=VERTEX_POINT('',#27471);
#7873=VERTEX_POINT('',#27473);
#7874=VERTEX_POINT('',#27475);
#7875=VERTEX_POINT('',#27477);
#7876=VERTEX_POINT('',#27479);
#7877=VERTEX_POINT('',#27481);
#7878=VERTEX_POINT('',#27483);
#7879=VERTEX_POINT('',#27487);
#7880=VERTEX_POINT('',#27489);
#7881=VERTEX_POINT('',#27493);
#7882=VERTEX_POINT('',#27497);
#7883=VERTEX_POINT('',#27501);
#7884=VERTEX_POINT('',#27504);
#7885=VERTEX_POINT('',#27506);
#7886=VERTEX_POINT('',#27509);
#7887=VERTEX_POINT('',#27513);
#7888=VERTEX_POINT('',#27517);
#7889=VERTEX_POINT('',#27519);
#7890=VERTEX_POINT('',#27521);
#7891=VERTEX_POINT('',#27523);
#7892=VERTEX_POINT('',#27525);
#7893=VERTEX_POINT('',#27527);
#7894=VERTEX_POINT('',#27529);
#7895=VERTEX_POINT('',#27531);
#7896=VERTEX_POINT('',#27533);
#7897=VERTEX_POINT('',#27535);
#7898=VERTEX_POINT('',#27537);
#7899=VERTEX_POINT('',#27539);
#7900=VERTEX_POINT('',#27541);
#7901=VERTEX_POINT('',#27543);
#7902=VERTEX_POINT('',#27545);
#7903=VERTEX_POINT('',#27547);
#7904=VERTEX_POINT('',#27549);
#7905=VERTEX_POINT('',#27551);
#7906=VERTEX_POINT('',#27553);
#7907=VERTEX_POINT('',#27555);
#7908=VERTEX_POINT('',#27557);
#7909=VERTEX_POINT('',#27560);
#7910=VERTEX_POINT('',#27562);
#7911=VERTEX_POINT('',#27564);
#7912=VERTEX_POINT('',#27566);
#7913=VERTEX_POINT('',#27568);
#7914=VERTEX_POINT('',#27570);
#7915=VERTEX_POINT('',#27572);
#7916=VERTEX_POINT('',#27574);
#7917=VERTEX_POINT('',#27586);
#7918=VERTEX_POINT('',#27588);
#7919=VERTEX_POINT('',#27592);
#7920=VERTEX_POINT('',#27596);
#7921=VERTEX_POINT('',#27600);
#7922=VERTEX_POINT('',#27604);
#7923=VERTEX_POINT('',#27658);
#7924=VERTEX_POINT('',#27659);
#7925=VERTEX_POINT('',#27661);
#7926=VERTEX_POINT('',#27663);
#7927=VERTEX_POINT('',#27667);
#7928=VERTEX_POINT('',#27669);
#7929=VERTEX_POINT('',#27673);
#7930=VERTEX_POINT('',#27675);
#7931=VERTEX_POINT('',#27679);
#7932=VERTEX_POINT('',#27681);
#7933=VERTEX_POINT('',#27685);
#7934=VERTEX_POINT('',#27687);
#7935=VERTEX_POINT('',#27691);
#7936=VERTEX_POINT('',#27693);
#7937=VERTEX_POINT('',#27697);
#7938=VERTEX_POINT('',#27699);
#7939=VERTEX_POINT('',#27703);
#7940=VERTEX_POINT('',#27705);
#7941=VERTEX_POINT('',#27709);
#7942=VERTEX_POINT('',#27710);
#7943=VERTEX_POINT('',#27712);
#7944=VERTEX_POINT('',#27714);
#7945=VERTEX_POINT('',#27718);
#7946=VERTEX_POINT('',#27720);
#7947=VERTEX_POINT('',#27724);
#7948=VERTEX_POINT('',#27726);
#7949=VERTEX_POINT('',#27730);
#7950=VERTEX_POINT('',#27732);
#7951=VERTEX_POINT('',#27736);
#7952=VERTEX_POINT('',#27738);
#7953=VERTEX_POINT('',#27742);
#7954=VERTEX_POINT('',#27744);
#7955=VERTEX_POINT('',#27748);
#7956=VERTEX_POINT('',#27750);
#7957=VERTEX_POINT('',#27754);
#7958=VERTEX_POINT('',#27756);
#7959=VERTEX_POINT('',#27760);
#7960=VERTEX_POINT('',#27761);
#7961=VERTEX_POINT('',#27763);
#7962=VERTEX_POINT('',#27765);
#7963=VERTEX_POINT('',#27767);
#7964=VERTEX_POINT('',#27769);
#7965=VERTEX_POINT('',#27771);
#7966=VERTEX_POINT('',#27773);
#7967=VERTEX_POINT('',#27775);
#7968=VERTEX_POINT('',#27777);
#7969=VERTEX_POINT('',#27779);
#7970=VERTEX_POINT('',#27781);
#7971=VERTEX_POINT('',#27783);
#7972=VERTEX_POINT('',#27785);
#7973=VERTEX_POINT('',#27787);
#7974=VERTEX_POINT('',#27789);
#7975=VERTEX_POINT('',#27791);
#7976=VERTEX_POINT('',#27793);
#7977=VERTEX_POINT('',#27801);
#7978=VERTEX_POINT('',#27805);
#7979=VERTEX_POINT('',#27809);
#7980=VERTEX_POINT('',#27813);
#7981=VERTEX_POINT('',#27817);
#7982=VERTEX_POINT('',#27821);
#7983=VERTEX_POINT('',#27825);
#7984=VERTEX_POINT('',#27829);
#7985=VERTEX_POINT('',#27833);
#7986=VERTEX_POINT('',#27837);
#7987=VERTEX_POINT('',#27841);
#7988=VERTEX_POINT('',#27845);
#7989=VERTEX_POINT('',#27849);
#7990=VERTEX_POINT('',#27853);
#7991=VERTEX_POINT('',#27857);
#7992=VERTEX_POINT('',#27861);
#7993=VERTEX_POINT('',#27865);
#7994=VERTEX_POINT('',#27869);
#9709=EDGE_CURVE('',#7755,#7756,#3993,.T.);
#9710=EDGE_CURVE('',#7756,#7757,#3994,.T.);
#9711=EDGE_CURVE('',#7757,#7758,#3995,.T.);
#9712=EDGE_CURVE('',#7758,#7759,#3996,.T.);
#9713=EDGE_CURVE('',#7759,#7760,#3389,.T.);
#9714=EDGE_CURVE('',#7760,#7761,#3997,.T.);
#9715=EDGE_CURVE('',#7761,#7762,#3390,.T.);
#9716=EDGE_CURVE('',#7762,#7763,#3998,.T.);
#9717=EDGE_CURVE('',#7763,#7764,#3391,.T.);
#9718=EDGE_CURVE('',#7764,#7765,#3392,.T.);
#9719=EDGE_CURVE('',#7765,#7766,#3393,.T.);
#9720=EDGE_CURVE('',#7766,#7767,#3999,.T.);
#9721=EDGE_CURVE('',#7767,#7768,#3394,.T.);
#9722=EDGE_CURVE('',#7768,#7769,#3395,.T.);
#9723=EDGE_CURVE('',#7769,#7770,#3396,.T.);
#9724=EDGE_CURVE('',#7770,#7771,#4000,.T.);
#9725=EDGE_CURVE('',#7771,#7772,#4001,.T.);
#9726=EDGE_CURVE('',#7772,#7773,#4002,.T.);
#9727=EDGE_CURVE('',#7773,#7774,#3397,.T.);
#9728=EDGE_CURVE('',#7774,#7775,#3398,.T.);
#9729=EDGE_CURVE('',#7775,#7776,#3399,.T.);
#9730=EDGE_CURVE('',#7776,#7777,#4003,.T.);
#9731=EDGE_CURVE('',#7777,#7778,#3400,.T.);
#9732=EDGE_CURVE('',#7778,#7779,#3401,.T.);
#9733=EDGE_CURVE('',#7779,#7780,#3402,.T.);
#9734=EDGE_CURVE('',#7780,#7781,#4004,.T.);
#9735=EDGE_CURVE('',#7781,#7782,#3403,.T.);
#9736=EDGE_CURVE('',#7782,#7783,#4005,.T.);
#9737=EDGE_CURVE('',#7783,#7784,#3404,.T.);
#9738=EDGE_CURVE('',#7784,#7785,#4006,.T.);
#9739=EDGE_CURVE('',#7785,#7786,#4007,.T.);
#9740=EDGE_CURVE('',#7786,#7787,#4008,.T.);
#9741=EDGE_CURVE('',#7787,#7788,#4009,.T.);
#9742=EDGE_CURVE('',#7788,#7789,#4010,.T.);
#9743=EDGE_CURVE('',#7789,#7790,#4011,.T.);
#9744=EDGE_CURVE('',#7790,#7755,#4012,.T.);
#9745=EDGE_CURVE('',#7772,#7791,#4013,.T.);
#9746=EDGE_CURVE('',#7791,#7792,#4014,.T.);
#9747=EDGE_CURVE('',#7773,#7792,#4015,.T.);
#9748=EDGE_CURVE('',#7792,#7793,#3405,.T.);
#9749=EDGE_CURVE('',#7774,#7793,#4016,.T.);
#9750=EDGE_CURVE('',#7793,#7794,#3406,.T.);
#9751=EDGE_CURVE('',#7775,#7794,#4017,.T.);
#9752=EDGE_CURVE('',#7794,#7795,#3407,.T.);
#9753=EDGE_CURVE('',#7776,#7795,#4018,.T.);
#9754=EDGE_CURVE('',#7795,#7796,#4019,.T.);
#9755=EDGE_CURVE('',#7777,#7796,#4020,.T.);
#9756=EDGE_CURVE('',#7796,#7797,#3408,.T.);
#9757=EDGE_CURVE('',#7778,#7797,#4021,.T.);
#9758=EDGE_CURVE('',#7797,#7798,#3409,.T.);
#9759=EDGE_CURVE('',#7779,#7798,#4022,.T.);
#9760=EDGE_CURVE('',#7798,#7799,#3410,.T.);
#9761=EDGE_CURVE('',#7780,#7799,#4023,.T.);
#9762=EDGE_CURVE('',#7799,#7800,#4024,.T.);
#9763=EDGE_CURVE('',#7781,#7800,#4025,.T.);
#9764=EDGE_CURVE('',#7800,#7801,#3411,.T.);
#9765=EDGE_CURVE('',#7782,#7801,#4026,.T.);
#9766=EDGE_CURVE('',#7801,#7802,#4027,.T.);
#9767=EDGE_CURVE('',#7783,#7802,#4028,.T.);
#9768=EDGE_CURVE('',#7802,#7803,#3412,.T.);
#9769=EDGE_CURVE('',#7784,#7803,#4029,.T.);
#9770=EDGE_CURVE('',#7803,#7804,#4030,.T.);
#9771=EDGE_CURVE('',#7785,#7804,#4031,.T.);
#9772=EDGE_CURVE('',#7804,#7805,#4032,.T.);
#9773=EDGE_CURVE('',#7786,#7805,#4033,.T.);
#9774=EDGE_CURVE('',#7805,#7806,#4034,.T.);
#9775=EDGE_CURVE('',#7787,#7806,#4035,.T.);
#9776=EDGE_CURVE('',#7806,#7807,#4036,.T.);
#9777=EDGE_CURVE('',#7788,#7807,#4037,.T.);
#9778=EDGE_CURVE('',#7755,#7808,#4038,.T.);
#9779=EDGE_CURVE('',#7808,#7809,#4039,.T.);
#9780=EDGE_CURVE('',#7756,#7809,#4040,.T.);
#9781=EDGE_CURVE('',#7809,#7810,#4041,.T.);
#9782=EDGE_CURVE('',#7757,#7810,#4042,.T.);
#9783=EDGE_CURVE('',#7810,#7811,#4043,.T.);
#9784=EDGE_CURVE('',#7758,#7811,#4044,.T.);
#9785=EDGE_CURVE('',#7811,#7812,#4045,.T.);
#9786=EDGE_CURVE('',#7759,#7812,#4046,.T.);
#9787=EDGE_CURVE('',#7812,#7813,#3413,.T.);
#9788=EDGE_CURVE('',#7760,#7813,#4047,.T.);
#9789=EDGE_CURVE('',#7807,#7814,#4048,.T.);
#9790=EDGE_CURVE('',#7789,#7814,#4049,.T.);
#9791=EDGE_CURVE('',#7814,#7815,#4050,.T.);
#9792=EDGE_CURVE('',#7790,#7815,#4051,.T.);
#9793=EDGE_CURVE('',#7815,#7808,#4052,.T.);
#9794=EDGE_CURVE('',#7813,#7816,#4053,.T.);
#9795=EDGE_CURVE('',#7816,#7761,#4054,.T.);
#9796=EDGE_CURVE('',#7771,#7817,#4055,.T.);
#9797=EDGE_CURVE('',#7817,#7791,#4056,.T.);
#9798=EDGE_CURVE('',#7770,#7818,#4057,.T.);
#9799=EDGE_CURVE('',#7818,#7817,#4058,.T.);
#9800=EDGE_CURVE('',#7769,#7819,#4059,.T.);
#9801=EDGE_CURVE('',#7819,#7818,#3414,.T.);
#9802=EDGE_CURVE('',#7768,#7820,#4060,.T.);
#9803=EDGE_CURVE('',#7820,#7819,#3415,.T.);
#9804=EDGE_CURVE('',#7767,#7821,#4061,.T.);
#9805=EDGE_CURVE('',#7821,#7820,#3416,.T.);
#9806=EDGE_CURVE('',#7766,#7822,#4062,.T.);
#9807=EDGE_CURVE('',#7822,#7821,#4063,.T.);
#9808=EDGE_CURVE('',#7765,#7823,#4064,.T.);
#9809=EDGE_CURVE('',#7823,#7822,#3417,.T.);
#9810=EDGE_CURVE('',#7764,#7824,#4065,.T.);
#9811=EDGE_CURVE('',#7824,#7823,#3418,.T.);
#9812=EDGE_CURVE('',#7763,#7825,#4066,.T.);
#9813=EDGE_CURVE('',#7825,#7824,#3419,.T.);
#9814=EDGE_CURVE('',#7762,#7826,#4067,.T.);
#9815=EDGE_CURVE('',#7826,#7825,#4068,.T.);
#9816=EDGE_CURVE('',#7816,#7826,#3420,.T.);
#9817=EDGE_CURVE('',#7827,#7828,#4069,.T.);
#9818=EDGE_CURVE('',#7829,#7828,#4070,.T.);
#9819=EDGE_CURVE('',#7830,#7829,#4071,.T.);
#9820=EDGE_CURVE('',#7830,#7827,#4072,.T.);
#9821=EDGE_CURVE('',#7828,#7831,#3421,.T.);
#9822=EDGE_CURVE('',#7832,#7831,#4073,.T.);
#9823=EDGE_CURVE('',#7829,#7832,#3422,.T.);
#9824=EDGE_CURVE('',#7831,#7833,#3423,.T.);
#9825=EDGE_CURVE('',#7834,#7833,#4074,.T.);
#9826=EDGE_CURVE('',#7832,#7834,#3424,.T.);
#9827=EDGE_CURVE('',#7833,#7835,#3425,.T.);
#9828=EDGE_CURVE('',#7836,#7835,#4075,.T.);
#9829=EDGE_CURVE('',#7834,#7836,#3426,.T.);
#9830=EDGE_CURVE('',#7835,#7837,#4076,.T.);
#9831=EDGE_CURVE('',#7838,#7837,#4077,.T.);
#9832=EDGE_CURVE('',#7836,#7838,#4078,.T.);
#9833=EDGE_CURVE('',#7837,#7839,#3427,.T.);
#9834=EDGE_CURVE('',#7840,#7839,#4079,.T.);
#9835=EDGE_CURVE('',#7838,#7840,#3428,.T.);
#9836=EDGE_CURVE('',#7839,#7841,#3429,.T.);
#9837=EDGE_CURVE('',#7842,#7841,#4080,.T.);
#9838=EDGE_CURVE('',#7840,#7842,#3430,.T.);
#9839=EDGE_CURVE('',#7843,#7844,#4081,.T.);
#9840=EDGE_CURVE('',#7845,#7843,#4082,.T.);
#9841=EDGE_CURVE('',#7846,#7845,#4083,.T.);
#9842=EDGE_CURVE('',#7847,#7846,#4084,.T.);
#9843=EDGE_CURVE('',#7848,#7847,#4085,.T.);
#9844=EDGE_CURVE('',#7849,#7848,#3431,.T.);
#9845=EDGE_CURVE('',#7850,#7849,#4086,.T.);
#9846=EDGE_CURVE('',#7851,#7850,#3432,.T.);
#9847=EDGE_CURVE('',#7852,#7851,#4087,.T.);
#9848=EDGE_CURVE('',#7841,#7852,#3433,.T.);
#9849=EDGE_CURVE('',#7853,#7827,#4088,.T.);
#9850=EDGE_CURVE('',#7854,#7853,#4089,.T.);
#9851=EDGE_CURVE('',#7855,#7854,#3434,.T.);
#9852=EDGE_CURVE('',#7856,#7855,#3435,.T.);
#9853=EDGE_CURVE('',#7857,#7856,#3436,.T.);
#9854=EDGE_CURVE('',#7858,#7857,#4090,.T.);
#9855=EDGE_CURVE('',#7859,#7858,#3437,.T.);
#9856=EDGE_CURVE('',#7860,#7859,#3438,.T.);
#9857=EDGE_CURVE('',#7861,#7860,#3439,.T.);
#9858=EDGE_CURVE('',#7862,#7861,#4091,.T.);
#9859=EDGE_CURVE('',#7863,#7862,#3440,.T.);
#9860=EDGE_CURVE('',#7864,#7863,#4092,.T.);
#9861=EDGE_CURVE('',#7865,#7864,#3441,.T.);
#9862=EDGE_CURVE('',#7866,#7865,#4093,.T.);
#9863=EDGE_CURVE('',#7867,#7866,#4094,.T.);
#9864=EDGE_CURVE('',#7868,#7867,#4095,.T.);
#9865=EDGE_CURVE('',#7869,#7868,#4096,.T.);
#9866=EDGE_CURVE('',#7869,#7870,#4097,.T.);
#9867=EDGE_CURVE('',#7870,#7871,#4098,.T.);
#9868=EDGE_CURVE('',#7871,#7872,#4099,.T.);
#9869=EDGE_CURVE('',#7872,#7873,#4100,.T.);
#9870=EDGE_CURVE('',#7873,#7874,#3442,.T.);
#9871=EDGE_CURVE('',#7875,#7874,#4101,.T.);
#9872=EDGE_CURVE('',#7876,#7875,#3443,.T.);
#9873=EDGE_CURVE('',#7877,#7876,#4102,.T.);
#9874=EDGE_CURVE('',#7878,#7877,#4103,.T.);
#9875=EDGE_CURVE('',#7844,#7878,#4104,.T.);
#9876=EDGE_CURVE('',#7879,#7844,#4105,.T.);
#9877=EDGE_CURVE('',#7879,#7880,#4106,.T.);
#9878=EDGE_CURVE('',#7880,#7843,#4107,.T.);
#9879=EDGE_CURVE('',#7881,#7878,#4108,.T.);
#9880=EDGE_CURVE('',#7881,#7879,#4109,.T.);
#9881=EDGE_CURVE('',#7882,#7877,#4110,.T.);
#9882=EDGE_CURVE('',#7882,#7881,#4111,.T.);
#9883=EDGE_CURVE('',#7883,#7876,#4112,.T.);
#9884=EDGE_CURVE('',#7883,#7882,#4113,.T.);
#9885=EDGE_CURVE('',#7884,#7884,#3444,.T.);
#9886=EDGE_CURVE('',#7885,#7885,#3445,.T.);
#9887=EDGE_CURVE('',#7886,#7875,#4114,.T.);
#9888=EDGE_CURVE('',#7886,#7883,#3446,.T.);
#9889=EDGE_CURVE('',#7887,#7874,#4115,.T.);
#9890=EDGE_CURVE('',#7886,#7887,#4116,.T.);
#9891=EDGE_CURVE('',#7887,#7888,#3447,.T.);
#9892=EDGE_CURVE('',#7888,#7889,#4117,.T.);
#9893=EDGE_CURVE('',#7889,#7890,#4118,.T.);
#9894=EDGE_CURVE('',#7890,#7891,#4119,.T.);
#9895=EDGE_CURVE('',#7891,#7892,#4120,.T.);
#9896=EDGE_CURVE('',#7892,#7893,#4121,.T.);
#9897=EDGE_CURVE('',#7893,#7894,#4122,.T.);
#9898=EDGE_CURVE('',#7894,#7895,#4123,.T.);
#9899=EDGE_CURVE('',#7895,#7896,#4124,.T.);
#9900=EDGE_CURVE('',#7896,#7897,#3448,.T.);
#9901=EDGE_CURVE('',#7897,#7898,#4125,.T.);
#9902=EDGE_CURVE('',#7898,#7899,#3449,.T.);
#9903=EDGE_CURVE('',#7899,#7900,#4126,.T.);
#9904=EDGE_CURVE('',#7900,#7901,#3450,.T.);
#9905=EDGE_CURVE('',#7901,#7902,#3451,.T.);
#9906=EDGE_CURVE('',#7902,#7903,#3452,.T.);
#9907=EDGE_CURVE('',#7903,#7904,#4127,.T.);
#9908=EDGE_CURVE('',#7904,#7905,#3453,.T.);
#9909=EDGE_CURVE('',#7905,#7906,#3454,.T.);
#9910=EDGE_CURVE('',#7906,#7907,#3455,.T.);
#9911=EDGE_CURVE('',#7907,#7908,#4128,.T.);
#9912=EDGE_CURVE('',#7908,#7830,#4129,.T.);
#9913=EDGE_CURVE('',#7842,#7909,#3456,.T.);
#9914=EDGE_CURVE('',#7909,#7910,#4130,.T.);
#9915=EDGE_CURVE('',#7910,#7911,#3457,.T.);
#9916=EDGE_CURVE('',#7911,#7912,#4131,.T.);
#9917=EDGE_CURVE('',#7912,#7913,#3458,.T.);
#9918=EDGE_CURVE('',#7913,#7914,#4132,.T.);
#9919=EDGE_CURVE('',#7914,#7915,#4133,.T.);
#9920=EDGE_CURVE('',#7915,#7916,#4134,.T.);
#9921=EDGE_CURVE('',#7916,#7880,#4135,.T.);
#9922=EDGE_CURVE('',#7891,#7870,#4136,.T.);
#9923=EDGE_CURVE('',#7869,#7892,#4137,.T.);
#9924=EDGE_CURVE('',#7890,#7871,#4138,.T.);
#9925=EDGE_CURVE('',#7889,#7872,#4139,.T.);
#9926=EDGE_CURVE('',#7888,#7873,#4140,.T.);
#9927=EDGE_CURVE('',#7917,#7917,#3459,.T.);
#9928=EDGE_CURVE('',#7918,#7918,#3460,.T.);
#9929=EDGE_CURVE('',#7885,#7919,#4141,.T.);
#9930=EDGE_CURVE('',#7919,#7919,#3461,.T.);
#9931=EDGE_CURVE('',#7918,#7920,#4142,.T.);
#9932=EDGE_CURVE('',#7920,#7920,#3462,.T.);
#9933=EDGE_CURVE('',#7884,#7921,#4143,.T.);
#9934=EDGE_CURVE('',#7921,#7921,#3463,.T.);
#9935=EDGE_CURVE('',#7917,#7922,#4144,.T.);
#9936=EDGE_CURVE('',#7922,#7922,#3464,.T.);
#9937=EDGE_CURVE('',#7916,#7845,#4145,.T.);
#9938=EDGE_CURVE('',#7915,#7846,#4146,.T.);
#9939=EDGE_CURVE('',#7914,#7847,#4147,.T.);
#9940=EDGE_CURVE('',#7913,#7848,#4148,.T.);
#9941=EDGE_CURVE('',#7912,#7849,#4149,.T.);
#9942=EDGE_CURVE('',#7911,#7850,#4150,.T.);
#9943=EDGE_CURVE('',#7910,#7851,#4151,.T.);
#9944=EDGE_CURVE('',#7909,#7852,#4152,.T.);
#9945=EDGE_CURVE('',#7893,#7868,#4153,.T.);
#9946=EDGE_CURVE('',#7894,#7867,#4154,.T.);
#9947=EDGE_CURVE('',#7895,#7866,#4155,.T.);
#9948=EDGE_CURVE('',#7896,#7865,#4156,.T.);
#9949=EDGE_CURVE('',#7897,#7864,#4157,.T.);
#9950=EDGE_CURVE('',#7863,#7898,#4158,.T.);
#9951=EDGE_CURVE('',#7899,#7862,#4159,.T.);
#9952=EDGE_CURVE('',#7900,#7861,#4160,.T.);
#9953=EDGE_CURVE('',#7901,#7860,#4161,.T.);
#9954=EDGE_CURVE('',#7902,#7859,#4162,.T.);
#9955=EDGE_CURVE('',#7903,#7858,#4163,.T.);
#9956=EDGE_CURVE('',#7904,#7857,#4164,.T.);
#9957=EDGE_CURVE('',#7905,#7856,#4165,.T.);
#9958=EDGE_CURVE('',#7906,#7855,#4166,.T.);
#9959=EDGE_CURVE('',#7907,#7854,#4167,.T.);
#9960=EDGE_CURVE('',#7908,#7853,#4168,.T.);
#9961=EDGE_CURVE('',#7923,#7924,#3465,.T.);
#9962=EDGE_CURVE('',#7925,#7924,#4169,.T.);
#9963=EDGE_CURVE('',#7925,#7926,#3466,.T.);
#9964=EDGE_CURVE('',#7926,#7923,#4170,.T.);
#9965=EDGE_CURVE('',#7924,#7927,#4171,.T.);
#9966=EDGE_CURVE('',#7928,#7927,#4172,.T.);
#9967=EDGE_CURVE('',#7928,#7925,#4173,.T.);
#9968=EDGE_CURVE('',#7927,#7929,#3467,.T.);
#9969=EDGE_CURVE('',#7930,#7929,#4174,.T.);
#9970=EDGE_CURVE('',#7930,#7928,#3468,.T.);
#9971=EDGE_CURVE('',#7929,#7931,#4175,.T.);
#9972=EDGE_CURVE('',#7932,#7931,#4176,.T.);
#9973=EDGE_CURVE('',#7932,#7930,#4177,.T.);
#9974=EDGE_CURVE('',#7931,#7933,#3469,.T.);
#9975=EDGE_CURVE('',#7934,#7933,#4178,.T.);
#9976=EDGE_CURVE('',#7934,#7932,#3470,.T.);
#9977=EDGE_CURVE('',#7933,#7935,#4179,.T.);
#9978=EDGE_CURVE('',#7936,#7935,#4180,.T.);
#9979=EDGE_CURVE('',#7936,#7934,#4181,.T.);
#9980=EDGE_CURVE('',#7935,#7937,#4182,.T.);
#9981=EDGE_CURVE('',#7938,#7937,#4183,.T.);
#9982=EDGE_CURVE('',#7938,#7936,#4184,.T.);
#9983=EDGE_CURVE('',#7937,#7939,#4185,.T.);
#9984=EDGE_CURVE('',#7940,#7939,#4186,.T.);
#9985=EDGE_CURVE('',#7940,#7938,#4187,.T.);
#9986=EDGE_CURVE('',#7941,#7942,#4188,.T.);
#9987=EDGE_CURVE('',#7943,#7941,#4189,.T.);
#9988=EDGE_CURVE('',#7943,#7944,#4190,.T.);
#9989=EDGE_CURVE('',#7944,#7942,#4191,.T.);
#9990=EDGE_CURVE('',#7945,#7941,#4192,.T.);
#9991=EDGE_CURVE('',#7946,#7945,#4193,.T.);
#9992=EDGE_CURVE('',#7946,#7943,#4194,.T.);
#9993=EDGE_CURVE('',#7947,#7945,#4195,.T.);
#9994=EDGE_CURVE('',#7948,#7947,#4196,.T.);
#9995=EDGE_CURVE('',#7948,#7946,#4197,.T.);
#9996=EDGE_CURVE('',#7947,#7949,#4198,.T.);
#9997=EDGE_CURVE('',#7950,#7949,#4199,.T.);
#9998=EDGE_CURVE('',#7950,#7948,#4200,.T.);
#9999=EDGE_CURVE('',#7949,#7951,#4201,.T.);
#10000=EDGE_CURVE('',#7952,#7951,#4202,.T.);
#10001=EDGE_CURVE('',#7952,#7950,#4203,.T.);
#10002=EDGE_CURVE('',#7951,#7953,#4204,.T.);
#10003=EDGE_CURVE('',#7954,#7953,#4205,.T.);
#10004=EDGE_CURVE('',#7954,#7952,#4206,.T.);
#10005=EDGE_CURVE('',#7953,#7955,#4207,.T.);
#10006=EDGE_CURVE('',#7956,#7955,#4208,.T.);
#10007=EDGE_CURVE('',#7956,#7954,#4209,.T.);
#10008=EDGE_CURVE('',#7955,#7957,#3471,.T.);
#10009=EDGE_CURVE('',#7958,#7957,#4210,.T.);
#10010=EDGE_CURVE('',#7958,#7956,#3472,.T.);
#10011=EDGE_CURVE('',#7959,#7960,#3473,.T.);
#10012=EDGE_CURVE('',#7961,#7959,#4211,.T.);
#10013=EDGE_CURVE('',#7962,#7961,#3474,.T.);
#10014=EDGE_CURVE('',#7963,#7962,#3475,.T.);
#10015=EDGE_CURVE('',#7964,#7963,#3476,.T.);
#10016=EDGE_CURVE('',#7965,#7964,#4212,.T.);
#10017=EDGE_CURVE('',#7966,#7965,#3477,.T.);
#10018=EDGE_CURVE('',#7967,#7966,#3478,.T.);
#10019=EDGE_CURVE('',#7968,#7967,#3479,.T.);
#10020=EDGE_CURVE('',#7969,#7968,#4213,.T.);
#10021=EDGE_CURVE('',#7970,#7969,#4214,.T.);
#10022=EDGE_CURVE('',#7971,#7970,#4215,.T.);
#10023=EDGE_CURVE('',#7972,#7971,#3480,.T.);
#10024=EDGE_CURVE('',#7973,#7972,#3481,.T.);
#10025=EDGE_CURVE('',#7974,#7973,#3482,.T.);
#10026=EDGE_CURVE('',#7975,#7974,#4216,.T.);
#10027=EDGE_CURVE('',#7976,#7975,#3483,.T.);
#10028=EDGE_CURVE('',#7926,#7976,#3484,.T.);
#10029=EDGE_CURVE('',#7944,#7940,#4217,.T.);
#10030=EDGE_CURVE('',#7960,#7958,#4218,.T.);
#10031=EDGE_CURVE('',#7939,#7942,#4219,.T.);
#10032=EDGE_CURVE('',#7957,#7977,#4220,.T.);
#10033=EDGE_CURVE('',#7977,#7960,#4221,.T.);
#10034=EDGE_CURVE('',#7977,#7978,#3485,.T.);
#10035=EDGE_CURVE('',#7959,#7978,#4222,.T.);
#10036=EDGE_CURVE('',#7978,#7979,#4223,.T.);
#10037=EDGE_CURVE('',#7961,#7979,#4224,.T.);
#10038=EDGE_CURVE('',#7979,#7980,#3486,.T.);
#10039=EDGE_CURVE('',#7962,#7980,#4225,.T.);
#10040=EDGE_CURVE('',#7980,#7981,#3487,.T.);
#10041=EDGE_CURVE('',#7963,#7981,#4226,.T.);
#10042=EDGE_CURVE('',#7981,#7982,#3488,.T.);
#10043=EDGE_CURVE('',#7964,#7982,#4227,.T.);
#10044=EDGE_CURVE('',#7982,#7983,#4228,.T.);
#10045=EDGE_CURVE('',#7965,#7983,#4229,.T.);
#10046=EDGE_CURVE('',#7983,#7984,#3489,.T.);
#10047=EDGE_CURVE('',#7966,#7984,#4230,.T.);
#10048=EDGE_CURVE('',#7984,#7985,#3490,.T.);
#10049=EDGE_CURVE('',#7967,#7985,#4231,.T.);
#10050=EDGE_CURVE('',#7985,#7986,#3491,.T.);
#10051=EDGE_CURVE('',#7968,#7986,#4232,.T.);
#10052=EDGE_CURVE('',#7986,#7987,#4233,.T.);
#10053=EDGE_CURVE('',#7969,#7987,#4234,.T.);
#10054=EDGE_CURVE('',#7987,#7988,#4235,.T.);
#10055=EDGE_CURVE('',#7970,#7988,#4236,.T.);
#10056=EDGE_CURVE('',#7988,#7989,#4237,.T.);
#10057=EDGE_CURVE('',#7971,#7989,#4238,.T.);
#10058=EDGE_CURVE('',#7989,#7990,#3492,.T.);
#10059=EDGE_CURVE('',#7972,#7990,#4239,.T.);
#10060=EDGE_CURVE('',#7990,#7991,#3493,.T.);
#10061=EDGE_CURVE('',#7973,#7991,#4240,.T.);
#10062=EDGE_CURVE('',#7991,#7992,#3494,.T.);
#10063=EDGE_CURVE('',#7974,#7992,#4241,.T.);
#10064=EDGE_CURVE('',#7992,#7993,#4242,.T.);
#10065=EDGE_CURVE('',#7975,#7993,#4243,.T.);
#10066=EDGE_CURVE('',#7993,#7994,#3495,.T.);
#10067=EDGE_CURVE('',#7976,#7994,#4244,.T.);
#10068=EDGE_CURVE('',#7994,#7923,#3496,.T.);
#12651=ORIENTED_EDGE('',*,*,#9709,.T.);
#12652=ORIENTED_EDGE('',*,*,#9710,.T.);
#12653=ORIENTED_EDGE('',*,*,#9711,.T.);
#12654=ORIENTED_EDGE('',*,*,#9712,.T.);
#12655=ORIENTED_EDGE('',*,*,#9713,.T.);
#12656=ORIENTED_EDGE('',*,*,#9714,.T.);
#12657=ORIENTED_EDGE('',*,*,#9715,.T.);
#12658=ORIENTED_EDGE('',*,*,#9716,.T.);
#12659=ORIENTED_EDGE('',*,*,#9717,.T.);
#12660=ORIENTED_EDGE('',*,*,#9718,.T.);
#12661=ORIENTED_EDGE('',*,*,#9719,.T.);
#12662=ORIENTED_EDGE('',*,*,#9720,.T.);
#12663=ORIENTED_EDGE('',*,*,#9721,.T.);
#12664=ORIENTED_EDGE('',*,*,#9722,.T.);
#12665=ORIENTED_EDGE('',*,*,#9723,.T.);
#12666=ORIENTED_EDGE('',*,*,#9724,.T.);
#12667=ORIENTED_EDGE('',*,*,#9725,.T.);
#12668=ORIENTED_EDGE('',*,*,#9726,.T.);
#12669=ORIENTED_EDGE('',*,*,#9727,.T.);
#12670=ORIENTED_EDGE('',*,*,#9728,.T.);
#12671=ORIENTED_EDGE('',*,*,#9729,.T.);
#12672=ORIENTED_EDGE('',*,*,#9730,.T.);
#12673=ORIENTED_EDGE('',*,*,#9731,.T.);
#12674=ORIENTED_EDGE('',*,*,#9732,.T.);
#12675=ORIENTED_EDGE('',*,*,#9733,.T.);
#12676=ORIENTED_EDGE('',*,*,#9734,.T.);
#12677=ORIENTED_EDGE('',*,*,#9735,.T.);
#12678=ORIENTED_EDGE('',*,*,#9736,.T.);
#12679=ORIENTED_EDGE('',*,*,#9737,.T.);
#12680=ORIENTED_EDGE('',*,*,#9738,.T.);
#12681=ORIENTED_EDGE('',*,*,#9739,.T.);
#12682=ORIENTED_EDGE('',*,*,#9740,.T.);
#12683=ORIENTED_EDGE('',*,*,#9741,.T.);
#12684=ORIENTED_EDGE('',*,*,#9742,.T.);
#12685=ORIENTED_EDGE('',*,*,#9743,.T.);
#12686=ORIENTED_EDGE('',*,*,#9744,.T.);
#12687=ORIENTED_EDGE('',*,*,#9726,.F.);
#12688=ORIENTED_EDGE('',*,*,#9745,.T.);
#12689=ORIENTED_EDGE('',*,*,#9746,.T.);
#12690=ORIENTED_EDGE('',*,*,#9747,.F.);
#12691=ORIENTED_EDGE('',*,*,#9727,.F.);
#12692=ORIENTED_EDGE('',*,*,#9747,.T.);
#12693=ORIENTED_EDGE('',*,*,#9748,.T.);
#12694=ORIENTED_EDGE('',*,*,#9749,.F.);
#12695=ORIENTED_EDGE('',*,*,#9728,.F.);
#12696=ORIENTED_EDGE('',*,*,#9749,.T.);
#12697=ORIENTED_EDGE('',*,*,#9750,.T.);
#12698=ORIENTED_EDGE('',*,*,#9751,.F.);
#12699=ORIENTED_EDGE('',*,*,#9729,.F.);
#12700=ORIENTED_EDGE('',*,*,#9751,.T.);
#12701=ORIENTED_EDGE('',*,*,#9752,.T.);
#12702=ORIENTED_EDGE('',*,*,#9753,.F.);
#12703=ORIENTED_EDGE('',*,*,#9730,.F.);
#12704=ORIENTED_EDGE('',*,*,#9753,.T.);
#12705=ORIENTED_EDGE('',*,*,#9754,.T.);
#12706=ORIENTED_EDGE('',*,*,#9755,.F.);
#12707=ORIENTED_EDGE('',*,*,#9731,.F.);
#12708=ORIENTED_EDGE('',*,*,#9755,.T.);
#12709=ORIENTED_EDGE('',*,*,#9756,.T.);
#12710=ORIENTED_EDGE('',*,*,#9757,.F.);
#12711=ORIENTED_EDGE('',*,*,#9732,.F.);
#12712=ORIENTED_EDGE('',*,*,#9757,.T.);
#12713=ORIENTED_EDGE('',*,*,#9758,.T.);
#12714=ORIENTED_EDGE('',*,*,#9759,.F.);
#12715=ORIENTED_EDGE('',*,*,#9733,.F.);
#12716=ORIENTED_EDGE('',*,*,#9759,.T.);
#12717=ORIENTED_EDGE('',*,*,#9760,.T.);
#12718=ORIENTED_EDGE('',*,*,#9761,.F.);
#12719=ORIENTED_EDGE('',*,*,#9734,.F.);
#12720=ORIENTED_EDGE('',*,*,#9761,.T.);
#12721=ORIENTED_EDGE('',*,*,#9762,.T.);
#12722=ORIENTED_EDGE('',*,*,#9763,.F.);
#12723=ORIENTED_EDGE('',*,*,#9735,.F.);
#12724=ORIENTED_EDGE('',*,*,#9763,.T.);
#12725=ORIENTED_EDGE('',*,*,#9764,.T.);
#12726=ORIENTED_EDGE('',*,*,#9765,.F.);
#12727=ORIENTED_EDGE('',*,*,#9736,.F.);
#12728=ORIENTED_EDGE('',*,*,#9765,.T.);
#12729=ORIENTED_EDGE('',*,*,#9766,.T.);
#12730=ORIENTED_EDGE('',*,*,#9767,.F.);
#12731=ORIENTED_EDGE('',*,*,#9737,.F.);
#12732=ORIENTED_EDGE('',*,*,#9767,.T.);
#12733=ORIENTED_EDGE('',*,*,#9768,.T.);
#12734=ORIENTED_EDGE('',*,*,#9769,.F.);
#12735=ORIENTED_EDGE('',*,*,#9738,.F.);
#12736=ORIENTED_EDGE('',*,*,#9769,.T.);
#12737=ORIENTED_EDGE('',*,*,#9770,.T.);
#12738=ORIENTED_EDGE('',*,*,#9771,.F.);
#12739=ORIENTED_EDGE('',*,*,#9739,.F.);
#12740=ORIENTED_EDGE('',*,*,#9771,.T.);
#12741=ORIENTED_EDGE('',*,*,#9772,.T.);
#12742=ORIENTED_EDGE('',*,*,#9773,.F.);
#12743=ORIENTED_EDGE('',*,*,#9740,.F.);
#12744=ORIENTED_EDGE('',*,*,#9773,.T.);
#12745=ORIENTED_EDGE('',*,*,#9774,.T.);
#12746=ORIENTED_EDGE('',*,*,#9775,.F.);
#12747=ORIENTED_EDGE('',*,*,#9741,.F.);
#12748=ORIENTED_EDGE('',*,*,#9775,.T.);
#12749=ORIENTED_EDGE('',*,*,#9776,.T.);
#12750=ORIENTED_EDGE('',*,*,#9777,.F.);
#12751=ORIENTED_EDGE('',*,*,#9709,.F.);
#12752=ORIENTED_EDGE('',*,*,#9778,.T.);
#12753=ORIENTED_EDGE('',*,*,#9779,.T.);
#12754=ORIENTED_EDGE('',*,*,#9780,.F.);
#12755=ORIENTED_EDGE('',*,*,#9710,.F.);
#12756=ORIENTED_EDGE('',*,*,#9780,.T.);
#12757=ORIENTED_EDGE('',*,*,#9781,.T.);
#12758=ORIENTED_EDGE('',*,*,#9782,.F.);
#12759=ORIENTED_EDGE('',*,*,#9711,.F.);
#12760=ORIENTED_EDGE('',*,*,#9782,.T.);
#12761=ORIENTED_EDGE('',*,*,#9783,.T.);
#12762=ORIENTED_EDGE('',*,*,#9784,.F.);
#12763=ORIENTED_EDGE('',*,*,#9712,.F.);
#12764=ORIENTED_EDGE('',*,*,#9784,.T.);
#12765=ORIENTED_EDGE('',*,*,#9785,.T.);
#12766=ORIENTED_EDGE('',*,*,#9786,.F.);
#12767=ORIENTED_EDGE('',*,*,#9713,.F.);
#12768=ORIENTED_EDGE('',*,*,#9786,.T.);
#12769=ORIENTED_EDGE('',*,*,#9787,.T.);
#12770=ORIENTED_EDGE('',*,*,#9788,.F.);
#12771=ORIENTED_EDGE('',*,*,#9742,.F.);
#12772=ORIENTED_EDGE('',*,*,#9777,.T.);
#12773=ORIENTED_EDGE('',*,*,#9789,.T.);
#12774=ORIENTED_EDGE('',*,*,#9790,.F.);
#12775=ORIENTED_EDGE('',*,*,#9743,.F.);
#12776=ORIENTED_EDGE('',*,*,#9790,.T.);
#12777=ORIENTED_EDGE('',*,*,#9791,.T.);
#12778=ORIENTED_EDGE('',*,*,#9792,.F.);
#12779=ORIENTED_EDGE('',*,*,#9744,.F.);
#12780=ORIENTED_EDGE('',*,*,#9792,.T.);
#12781=ORIENTED_EDGE('',*,*,#9793,.T.);
#12782=ORIENTED_EDGE('',*,*,#9778,.F.);
#12783=ORIENTED_EDGE('',*,*,#9714,.F.);
#12784=ORIENTED_EDGE('',*,*,#9788,.T.);
#12785=ORIENTED_EDGE('',*,*,#9794,.T.);
#12786=ORIENTED_EDGE('',*,*,#9795,.T.);
#12787=ORIENTED_EDGE('',*,*,#9725,.F.);
#12788=ORIENTED_EDGE('',*,*,#9796,.T.);
#12789=ORIENTED_EDGE('',*,*,#9797,.T.);
#12790=ORIENTED_EDGE('',*,*,#9745,.F.);
#12791=ORIENTED_EDGE('',*,*,#9724,.F.);
#12792=ORIENTED_EDGE('',*,*,#9798,.T.);
#12793=ORIENTED_EDGE('',*,*,#9799,.T.);
#12794=ORIENTED_EDGE('',*,*,#9796,.F.);
#12795=ORIENTED_EDGE('',*,*,#9723,.F.);
#12796=ORIENTED_EDGE('',*,*,#9800,.T.);
#12797=ORIENTED_EDGE('',*,*,#9801,.T.);
#12798=ORIENTED_EDGE('',*,*,#9798,.F.);
#12799=ORIENTED_EDGE('',*,*,#9722,.F.);
#12800=ORIENTED_EDGE('',*,*,#9802,.T.);
#12801=ORIENTED_EDGE('',*,*,#9803,.T.);
#12802=ORIENTED_EDGE('',*,*,#9800,.F.);
#12803=ORIENTED_EDGE('',*,*,#9721,.F.);
#12804=ORIENTED_EDGE('',*,*,#9804,.T.);
#12805=ORIENTED_EDGE('',*,*,#9805,.T.);
#12806=ORIENTED_EDGE('',*,*,#9802,.F.);
#12807=ORIENTED_EDGE('',*,*,#9720,.F.);
#12808=ORIENTED_EDGE('',*,*,#9806,.T.);
#12809=ORIENTED_EDGE('',*,*,#9807,.T.);
#12810=ORIENTED_EDGE('',*,*,#9804,.F.);
#12811=ORIENTED_EDGE('',*,*,#9719,.F.);
#12812=ORIENTED_EDGE('',*,*,#9808,.T.);
#12813=ORIENTED_EDGE('',*,*,#9809,.T.);
#12814=ORIENTED_EDGE('',*,*,#9806,.F.);
#12815=ORIENTED_EDGE('',*,*,#9718,.F.);
#12816=ORIENTED_EDGE('',*,*,#9810,.T.);
#12817=ORIENTED_EDGE('',*,*,#9811,.T.);
#12818=ORIENTED_EDGE('',*,*,#9808,.F.);
#12819=ORIENTED_EDGE('',*,*,#9717,.F.);
#12820=ORIENTED_EDGE('',*,*,#9812,.T.);
#12821=ORIENTED_EDGE('',*,*,#9813,.T.);
#12822=ORIENTED_EDGE('',*,*,#9810,.F.);
#12823=ORIENTED_EDGE('',*,*,#9716,.F.);
#12824=ORIENTED_EDGE('',*,*,#9814,.T.);
#12825=ORIENTED_EDGE('',*,*,#9815,.T.);
#12826=ORIENTED_EDGE('',*,*,#9812,.F.);
#12827=ORIENTED_EDGE('',*,*,#9715,.F.);
#12828=ORIENTED_EDGE('',*,*,#9795,.F.);
#12829=ORIENTED_EDGE('',*,*,#9816,.T.);
#12830=ORIENTED_EDGE('',*,*,#9814,.F.);
#12831=ORIENTED_EDGE('',*,*,#9816,.F.);
#12832=ORIENTED_EDGE('',*,*,#9794,.F.);
#12833=ORIENTED_EDGE('',*,*,#9787,.F.);
#12834=ORIENTED_EDGE('',*,*,#9785,.F.);
#12835=ORIENTED_EDGE('',*,*,#9783,.F.);
#12836=ORIENTED_EDGE('',*,*,#9781,.F.);
#12837=ORIENTED_EDGE('',*,*,#9779,.F.);
#12838=ORIENTED_EDGE('',*,*,#9793,.F.);
#12839=ORIENTED_EDGE('',*,*,#9791,.F.);
#12840=ORIENTED_EDGE('',*,*,#9789,.F.);
#12841=ORIENTED_EDGE('',*,*,#9776,.F.);
#12842=ORIENTED_EDGE('',*,*,#9774,.F.);
#12843=ORIENTED_EDGE('',*,*,#9772,.F.);
#12844=ORIENTED_EDGE('',*,*,#9770,.F.);
#12845=ORIENTED_EDGE('',*,*,#9768,.F.);
#12846=ORIENTED_EDGE('',*,*,#9766,.F.);
#12847=ORIENTED_EDGE('',*,*,#9764,.F.);
#12848=ORIENTED_EDGE('',*,*,#9762,.F.);
#12849=ORIENTED_EDGE('',*,*,#9760,.F.);
#12850=ORIENTED_EDGE('',*,*,#9758,.F.);
#12851=ORIENTED_EDGE('',*,*,#9756,.F.);
#12852=ORIENTED_EDGE('',*,*,#9754,.F.);
#12853=ORIENTED_EDGE('',*,*,#9752,.F.);
#12854=ORIENTED_EDGE('',*,*,#9750,.F.);
#12855=ORIENTED_EDGE('',*,*,#9748,.F.);
#12856=ORIENTED_EDGE('',*,*,#9746,.F.);
#12857=ORIENTED_EDGE('',*,*,#9797,.F.);
#12858=ORIENTED_EDGE('',*,*,#9799,.F.);
#12859=ORIENTED_EDGE('',*,*,#9801,.F.);
#12860=ORIENTED_EDGE('',*,*,#9803,.F.);
#12861=ORIENTED_EDGE('',*,*,#9805,.F.);
#12862=ORIENTED_EDGE('',*,*,#9807,.F.);
#12863=ORIENTED_EDGE('',*,*,#9809,.F.);
#12864=ORIENTED_EDGE('',*,*,#9811,.F.);
#12865=ORIENTED_EDGE('',*,*,#9813,.F.);
#12866=ORIENTED_EDGE('',*,*,#9815,.F.);
#12867=ORIENTED_EDGE('',*,*,#9817,.T.);
#12868=ORIENTED_EDGE('',*,*,#9818,.F.);
#12869=ORIENTED_EDGE('',*,*,#9819,.F.);
#12870=ORIENTED_EDGE('',*,*,#9820,.T.);
#12871=ORIENTED_EDGE('',*,*,#9821,.T.);
#12872=ORIENTED_EDGE('',*,*,#9822,.F.);
#12873=ORIENTED_EDGE('',*,*,#9823,.F.);
#12874=ORIENTED_EDGE('',*,*,#9818,.T.);
#12875=ORIENTED_EDGE('',*,*,#9824,.T.);
#12876=ORIENTED_EDGE('',*,*,#9825,.F.);
#12877=ORIENTED_EDGE('',*,*,#9826,.F.);
#12878=ORIENTED_EDGE('',*,*,#9822,.T.);
#12879=ORIENTED_EDGE('',*,*,#9827,.T.);
#12880=ORIENTED_EDGE('',*,*,#9828,.F.);
#12881=ORIENTED_EDGE('',*,*,#9829,.F.);
#12882=ORIENTED_EDGE('',*,*,#9825,.T.);
#12883=ORIENTED_EDGE('',*,*,#9830,.T.);
#12884=ORIENTED_EDGE('',*,*,#9831,.F.);
#12885=ORIENTED_EDGE('',*,*,#9832,.F.);
#12886=ORIENTED_EDGE('',*,*,#9828,.T.);
#12887=ORIENTED_EDGE('',*,*,#9833,.T.);
#12888=ORIENTED_EDGE('',*,*,#9834,.F.);
#12889=ORIENTED_EDGE('',*,*,#9835,.F.);
#12890=ORIENTED_EDGE('',*,*,#9831,.T.);
#12891=ORIENTED_EDGE('',*,*,#9836,.T.);
#12892=ORIENTED_EDGE('',*,*,#9837,.F.);
#12893=ORIENTED_EDGE('',*,*,#9838,.F.);
#12894=ORIENTED_EDGE('',*,*,#9834,.T.);
#12895=ORIENTED_EDGE('',*,*,#9839,.F.);
#12896=ORIENTED_EDGE('',*,*,#9840,.F.);
#12897=ORIENTED_EDGE('',*,*,#9841,.F.);
#12898=ORIENTED_EDGE('',*,*,#9842,.F.);
#12899=ORIENTED_EDGE('',*,*,#9843,.F.);
#12900=ORIENTED_EDGE('',*,*,#9844,.F.);
#12901=ORIENTED_EDGE('',*,*,#9845,.F.);
#12902=ORIENTED_EDGE('',*,*,#9846,.F.);
#12903=ORIENTED_EDGE('',*,*,#9847,.F.);
#12904=ORIENTED_EDGE('',*,*,#9848,.F.);
#12905=ORIENTED_EDGE('',*,*,#9836,.F.);
#12906=ORIENTED_EDGE('',*,*,#9833,.F.);
#12907=ORIENTED_EDGE('',*,*,#9830,.F.);
#12908=ORIENTED_EDGE('',*,*,#9827,.F.);
#12909=ORIENTED_EDGE('',*,*,#9824,.F.);
#12910=ORIENTED_EDGE('',*,*,#9821,.F.);
#12911=ORIENTED_EDGE('',*,*,#9817,.F.);
#12912=ORIENTED_EDGE('',*,*,#9849,.F.);
#12913=ORIENTED_EDGE('',*,*,#9850,.F.);
#12914=ORIENTED_EDGE('',*,*,#9851,.F.);
#12915=ORIENTED_EDGE('',*,*,#9852,.F.);
#12916=ORIENTED_EDGE('',*,*,#9853,.F.);
#12917=ORIENTED_EDGE('',*,*,#9854,.F.);
#12918=ORIENTED_EDGE('',*,*,#9855,.F.);
#12919=ORIENTED_EDGE('',*,*,#9856,.F.);
#12920=ORIENTED_EDGE('',*,*,#9857,.F.);
#12921=ORIENTED_EDGE('',*,*,#9858,.F.);
#12922=ORIENTED_EDGE('',*,*,#9859,.F.);
#12923=ORIENTED_EDGE('',*,*,#9860,.F.);
#12924=ORIENTED_EDGE('',*,*,#9861,.F.);
#12925=ORIENTED_EDGE('',*,*,#9862,.F.);
#12926=ORIENTED_EDGE('',*,*,#9863,.F.);
#12927=ORIENTED_EDGE('',*,*,#9864,.F.);
#12928=ORIENTED_EDGE('',*,*,#9865,.F.);
#12929=ORIENTED_EDGE('',*,*,#9866,.T.);
#12930=ORIENTED_EDGE('',*,*,#9867,.T.);
#12931=ORIENTED_EDGE('',*,*,#9868,.T.);
#12932=ORIENTED_EDGE('',*,*,#9869,.T.);
#12933=ORIENTED_EDGE('',*,*,#9870,.T.);
#12934=ORIENTED_EDGE('',*,*,#9871,.F.);
#12935=ORIENTED_EDGE('',*,*,#9872,.F.);
#12936=ORIENTED_EDGE('',*,*,#9873,.F.);
#12937=ORIENTED_EDGE('',*,*,#9874,.F.);
#12938=ORIENTED_EDGE('',*,*,#9875,.F.);
#12939=ORIENTED_EDGE('',*,*,#9876,.F.);
#12940=ORIENTED_EDGE('',*,*,#9877,.T.);
#12941=ORIENTED_EDGE('',*,*,#9878,.T.);
#12942=ORIENTED_EDGE('',*,*,#9839,.T.);
#12943=ORIENTED_EDGE('',*,*,#9879,.F.);
#12944=ORIENTED_EDGE('',*,*,#9880,.T.);
#12945=ORIENTED_EDGE('',*,*,#9876,.T.);
#12946=ORIENTED_EDGE('',*,*,#9875,.T.);
#12947=ORIENTED_EDGE('',*,*,#9881,.F.);
#12948=ORIENTED_EDGE('',*,*,#9882,.T.);
#12949=ORIENTED_EDGE('',*,*,#9879,.T.);
#12950=ORIENTED_EDGE('',*,*,#9874,.T.);
#12951=ORIENTED_EDGE('',*,*,#9883,.F.);
#12952=ORIENTED_EDGE('',*,*,#9884,.T.);
#12953=ORIENTED_EDGE('',*,*,#9881,.T.);
#12954=ORIENTED_EDGE('',*,*,#9873,.T.);
#12955=ORIENTED_EDGE('',*,*,#9885,.F.);
#12956=ORIENTED_EDGE('',*,*,#9886,.F.);
#12957=ORIENTED_EDGE('',*,*,#9887,.F.);
#12958=ORIENTED_EDGE('',*,*,#9888,.T.);
#12959=ORIENTED_EDGE('',*,*,#9883,.T.);
#12960=ORIENTED_EDGE('',*,*,#9872,.T.);
#12961=ORIENTED_EDGE('',*,*,#9871,.T.);
#12962=ORIENTED_EDGE('',*,*,#9889,.F.);
#12963=ORIENTED_EDGE('',*,*,#9890,.F.);
#12964=ORIENTED_EDGE('',*,*,#9887,.T.);
#12965=ORIENTED_EDGE('',*,*,#9877,.F.);
#12966=ORIENTED_EDGE('',*,*,#9880,.F.);
#12967=ORIENTED_EDGE('',*,*,#9882,.F.);
#12968=ORIENTED_EDGE('',*,*,#9884,.F.);
#12969=ORIENTED_EDGE('',*,*,#9888,.F.);
#12970=ORIENTED_EDGE('',*,*,#9890,.T.);
#12971=ORIENTED_EDGE('',*,*,#9891,.T.);
#12972=ORIENTED_EDGE('',*,*,#9892,.T.);
#12973=ORIENTED_EDGE('',*,*,#9893,.T.);
#12974=ORIENTED_EDGE('',*,*,#9894,.T.);
#12975=ORIENTED_EDGE('',*,*,#9895,.T.);
#12976=ORIENTED_EDGE('',*,*,#9896,.T.);
#12977=ORIENTED_EDGE('',*,*,#9897,.T.);
#12978=ORIENTED_EDGE('',*,*,#9898,.T.);
#12979=ORIENTED_EDGE('',*,*,#9899,.T.);
#12980=ORIENTED_EDGE('',*,*,#9900,.T.);
#12981=ORIENTED_EDGE('',*,*,#9901,.T.);
#12982=ORIENTED_EDGE('',*,*,#9902,.T.);
#12983=ORIENTED_EDGE('',*,*,#9903,.T.);
#12984=ORIENTED_EDGE('',*,*,#9904,.T.);
#12985=ORIENTED_EDGE('',*,*,#9905,.T.);
#12986=ORIENTED_EDGE('',*,*,#9906,.T.);
#12987=ORIENTED_EDGE('',*,*,#9907,.T.);
#12988=ORIENTED_EDGE('',*,*,#9908,.T.);
#12989=ORIENTED_EDGE('',*,*,#9909,.T.);
#12990=ORIENTED_EDGE('',*,*,#9910,.T.);
#12991=ORIENTED_EDGE('',*,*,#9911,.T.);
#12992=ORIENTED_EDGE('',*,*,#9912,.T.);
#12993=ORIENTED_EDGE('',*,*,#9819,.T.);
#12994=ORIENTED_EDGE('',*,*,#9823,.T.);
#12995=ORIENTED_EDGE('',*,*,#9826,.T.);
#12996=ORIENTED_EDGE('',*,*,#9829,.T.);
#12997=ORIENTED_EDGE('',*,*,#9832,.T.);
#12998=ORIENTED_EDGE('',*,*,#9835,.T.);
#12999=ORIENTED_EDGE('',*,*,#9838,.T.);
#13000=ORIENTED_EDGE('',*,*,#9913,.T.);
#13001=ORIENTED_EDGE('',*,*,#9914,.T.);
#13002=ORIENTED_EDGE('',*,*,#9915,.T.);
#13003=ORIENTED_EDGE('',*,*,#9916,.T.);
#13004=ORIENTED_EDGE('',*,*,#9917,.T.);
#13005=ORIENTED_EDGE('',*,*,#9918,.T.);
#13006=ORIENTED_EDGE('',*,*,#9919,.T.);
#13007=ORIENTED_EDGE('',*,*,#9920,.T.);
#13008=ORIENTED_EDGE('',*,*,#9921,.T.);
#13009=ORIENTED_EDGE('',*,*,#9922,.T.);
#13010=ORIENTED_EDGE('',*,*,#9866,.F.);
#13011=ORIENTED_EDGE('',*,*,#9923,.T.);
#13012=ORIENTED_EDGE('',*,*,#9895,.F.);
#13013=ORIENTED_EDGE('',*,*,#9924,.T.);
#13014=ORIENTED_EDGE('',*,*,#9867,.F.);
#13015=ORIENTED_EDGE('',*,*,#9922,.F.);
#13016=ORIENTED_EDGE('',*,*,#9894,.F.);
#13017=ORIENTED_EDGE('',*,*,#9925,.T.);
#13018=ORIENTED_EDGE('',*,*,#9868,.F.);
#13019=ORIENTED_EDGE('',*,*,#9924,.F.);
#13020=ORIENTED_EDGE('',*,*,#9893,.F.);
#13021=ORIENTED_EDGE('',*,*,#9926,.T.);
#13022=ORIENTED_EDGE('',*,*,#9869,.F.);
#13023=ORIENTED_EDGE('',*,*,#9925,.F.);
#13024=ORIENTED_EDGE('',*,*,#9892,.F.);
#13025=ORIENTED_EDGE('',*,*,#9927,.F.);
#13026=ORIENTED_EDGE('',*,*,#9928,.F.);
#13027=ORIENTED_EDGE('',*,*,#9889,.T.);
#13028=ORIENTED_EDGE('',*,*,#9870,.F.);
#13029=ORIENTED_EDGE('',*,*,#9926,.F.);
#13030=ORIENTED_EDGE('',*,*,#9891,.F.);
#13031=ORIENTED_EDGE('',*,*,#9886,.T.);
#13032=ORIENTED_EDGE('',*,*,#9929,.T.);
#13033=ORIENTED_EDGE('',*,*,#9930,.T.);
#13034=ORIENTED_EDGE('',*,*,#9929,.F.);
#13035=ORIENTED_EDGE('',*,*,#9928,.T.);
#13036=ORIENTED_EDGE('',*,*,#9931,.T.);
#13037=ORIENTED_EDGE('',*,*,#9932,.T.);
#13038=ORIENTED_EDGE('',*,*,#9931,.F.);
#13039=ORIENTED_EDGE('',*,*,#9885,.T.);
#13040=ORIENTED_EDGE('',*,*,#9933,.T.);
#13041=ORIENTED_EDGE('',*,*,#9934,.T.);
#13042=ORIENTED_EDGE('',*,*,#9933,.F.);
#13043=ORIENTED_EDGE('',*,*,#9927,.T.);
#13044=ORIENTED_EDGE('',*,*,#9935,.T.);
#13045=ORIENTED_EDGE('',*,*,#9936,.T.);
#13046=ORIENTED_EDGE('',*,*,#9935,.F.);
#13047=ORIENTED_EDGE('',*,*,#9840,.T.);
#13048=ORIENTED_EDGE('',*,*,#9878,.F.);
#13049=ORIENTED_EDGE('',*,*,#9921,.F.);
#13050=ORIENTED_EDGE('',*,*,#9937,.T.);
#13051=ORIENTED_EDGE('',*,*,#9841,.T.);
#13052=ORIENTED_EDGE('',*,*,#9937,.F.);
#13053=ORIENTED_EDGE('',*,*,#9920,.F.);
#13054=ORIENTED_EDGE('',*,*,#9938,.T.);
#13055=ORIENTED_EDGE('',*,*,#9842,.T.);
#13056=ORIENTED_EDGE('',*,*,#9938,.F.);
#13057=ORIENTED_EDGE('',*,*,#9919,.F.);
#13058=ORIENTED_EDGE('',*,*,#9939,.T.);
#13059=ORIENTED_EDGE('',*,*,#9930,.F.);
#13060=ORIENTED_EDGE('',*,*,#9934,.F.);
#13061=ORIENTED_EDGE('',*,*,#9843,.T.);
#13062=ORIENTED_EDGE('',*,*,#9939,.F.);
#13063=ORIENTED_EDGE('',*,*,#9918,.F.);
#13064=ORIENTED_EDGE('',*,*,#9940,.T.);
#13065=ORIENTED_EDGE('',*,*,#9844,.T.);
#13066=ORIENTED_EDGE('',*,*,#9940,.F.);
#13067=ORIENTED_EDGE('',*,*,#9917,.F.);
#13068=ORIENTED_EDGE('',*,*,#9941,.T.);
#13069=ORIENTED_EDGE('',*,*,#9845,.T.);
#13070=ORIENTED_EDGE('',*,*,#9941,.F.);
#13071=ORIENTED_EDGE('',*,*,#9916,.F.);
#13072=ORIENTED_EDGE('',*,*,#9942,.T.);
#13073=ORIENTED_EDGE('',*,*,#9846,.T.);
#13074=ORIENTED_EDGE('',*,*,#9942,.F.);
#13075=ORIENTED_EDGE('',*,*,#9915,.F.);
#13076=ORIENTED_EDGE('',*,*,#9943,.T.);
#13077=ORIENTED_EDGE('',*,*,#9847,.T.);
#13078=ORIENTED_EDGE('',*,*,#9943,.F.);
#13079=ORIENTED_EDGE('',*,*,#9914,.F.);
#13080=ORIENTED_EDGE('',*,*,#9944,.T.);
#13081=ORIENTED_EDGE('',*,*,#9848,.T.);
#13082=ORIENTED_EDGE('',*,*,#9944,.F.);
#13083=ORIENTED_EDGE('',*,*,#9913,.F.);
#13084=ORIENTED_EDGE('',*,*,#9837,.T.);
#13085=ORIENTED_EDGE('',*,*,#9865,.T.);
#13086=ORIENTED_EDGE('',*,*,#9945,.F.);
#13087=ORIENTED_EDGE('',*,*,#9896,.F.);
#13088=ORIENTED_EDGE('',*,*,#9923,.F.);
#13089=ORIENTED_EDGE('',*,*,#9864,.T.);
#13090=ORIENTED_EDGE('',*,*,#9946,.F.);
#13091=ORIENTED_EDGE('',*,*,#9897,.F.);
#13092=ORIENTED_EDGE('',*,*,#9945,.T.);
#13093=ORIENTED_EDGE('',*,*,#9863,.T.);
#13094=ORIENTED_EDGE('',*,*,#9947,.F.);
#13095=ORIENTED_EDGE('',*,*,#9898,.F.);
#13096=ORIENTED_EDGE('',*,*,#9946,.T.);
#13097=ORIENTED_EDGE('',*,*,#9936,.F.);
#13098=ORIENTED_EDGE('',*,*,#9932,.F.);
#13099=ORIENTED_EDGE('',*,*,#9862,.T.);
#13100=ORIENTED_EDGE('',*,*,#9948,.F.);
#13101=ORIENTED_EDGE('',*,*,#9899,.F.);
#13102=ORIENTED_EDGE('',*,*,#9947,.T.);
#13103=ORIENTED_EDGE('',*,*,#9861,.T.);
#13104=ORIENTED_EDGE('',*,*,#9949,.F.);
#13105=ORIENTED_EDGE('',*,*,#9900,.F.);
#13106=ORIENTED_EDGE('',*,*,#9948,.T.);
#13107=ORIENTED_EDGE('',*,*,#9860,.T.);
#13108=ORIENTED_EDGE('',*,*,#9950,.T.);
#13109=ORIENTED_EDGE('',*,*,#9901,.F.);
#13110=ORIENTED_EDGE('',*,*,#9949,.T.);
#13111=ORIENTED_EDGE('',*,*,#9859,.T.);
#13112=ORIENTED_EDGE('',*,*,#9951,.F.);
#13113=ORIENTED_EDGE('',*,*,#9902,.F.);
#13114=ORIENTED_EDGE('',*,*,#9950,.F.);
#13115=ORIENTED_EDGE('',*,*,#9858,.T.);
#13116=ORIENTED_EDGE('',*,*,#9952,.F.);
#13117=ORIENTED_EDGE('',*,*,#9903,.F.);
#13118=ORIENTED_EDGE('',*,*,#9951,.T.);
#13119=ORIENTED_EDGE('',*,*,#9857,.T.);
#13120=ORIENTED_EDGE('',*,*,#9953,.F.);
#13121=ORIENTED_EDGE('',*,*,#9904,.F.);
#13122=ORIENTED_EDGE('',*,*,#9952,.T.);
#13123=ORIENTED_EDGE('',*,*,#9856,.T.);
#13124=ORIENTED_EDGE('',*,*,#9954,.F.);
#13125=ORIENTED_EDGE('',*,*,#9905,.F.);
#13126=ORIENTED_EDGE('',*,*,#9953,.T.);
#13127=ORIENTED_EDGE('',*,*,#9855,.T.);
#13128=ORIENTED_EDGE('',*,*,#9955,.F.);
#13129=ORIENTED_EDGE('',*,*,#9906,.F.);
#13130=ORIENTED_EDGE('',*,*,#9954,.T.);
#13131=ORIENTED_EDGE('',*,*,#9854,.T.);
#13132=ORIENTED_EDGE('',*,*,#9956,.F.);
#13133=ORIENTED_EDGE('',*,*,#9907,.F.);
#13134=ORIENTED_EDGE('',*,*,#9955,.T.);
#13135=ORIENTED_EDGE('',*,*,#9853,.T.);
#13136=ORIENTED_EDGE('',*,*,#9957,.F.);
#13137=ORIENTED_EDGE('',*,*,#9908,.F.);
#13138=ORIENTED_EDGE('',*,*,#9956,.T.);
#13139=ORIENTED_EDGE('',*,*,#9852,.T.);
#13140=ORIENTED_EDGE('',*,*,#9958,.F.);
#13141=ORIENTED_EDGE('',*,*,#9909,.F.);
#13142=ORIENTED_EDGE('',*,*,#9957,.T.);
#13143=ORIENTED_EDGE('',*,*,#9851,.T.);
#13144=ORIENTED_EDGE('',*,*,#9959,.F.);
#13145=ORIENTED_EDGE('',*,*,#9910,.F.);
#13146=ORIENTED_EDGE('',*,*,#9958,.T.);
#13147=ORIENTED_EDGE('',*,*,#9850,.T.);
#13148=ORIENTED_EDGE('',*,*,#9960,.F.);
#13149=ORIENTED_EDGE('',*,*,#9911,.F.);
#13150=ORIENTED_EDGE('',*,*,#9959,.T.);
#13151=ORIENTED_EDGE('',*,*,#9849,.T.);
#13152=ORIENTED_EDGE('',*,*,#9820,.F.);
#13153=ORIENTED_EDGE('',*,*,#9912,.F.);
#13154=ORIENTED_EDGE('',*,*,#9960,.T.);
#13155=ORIENTED_EDGE('',*,*,#9961,.T.);
#13156=ORIENTED_EDGE('',*,*,#9962,.F.);
#13157=ORIENTED_EDGE('',*,*,#9963,.T.);
#13158=ORIENTED_EDGE('',*,*,#9964,.T.);
#13159=ORIENTED_EDGE('',*,*,#9965,.T.);
#13160=ORIENTED_EDGE('',*,*,#9966,.F.);
#13161=ORIENTED_EDGE('',*,*,#9967,.T.);
#13162=ORIENTED_EDGE('',*,*,#9962,.T.);
#13163=ORIENTED_EDGE('',*,*,#9968,.T.);
#13164=ORIENTED_EDGE('',*,*,#9969,.F.);
#13165=ORIENTED_EDGE('',*,*,#9970,.T.);
#13166=ORIENTED_EDGE('',*,*,#9966,.T.);
#13167=ORIENTED_EDGE('',*,*,#9971,.T.);
#13168=ORIENTED_EDGE('',*,*,#9972,.F.);
#13169=ORIENTED_EDGE('',*,*,#9973,.T.);
#13170=ORIENTED_EDGE('',*,*,#9969,.T.);
#13171=ORIENTED_EDGE('',*,*,#9974,.T.);
#13172=ORIENTED_EDGE('',*,*,#9975,.F.);
#13173=ORIENTED_EDGE('',*,*,#9976,.T.);
#13174=ORIENTED_EDGE('',*,*,#9972,.T.);
#13175=ORIENTED_EDGE('',*,*,#9977,.T.);
#13176=ORIENTED_EDGE('',*,*,#9978,.F.);
#13177=ORIENTED_EDGE('',*,*,#9979,.T.);
#13178=ORIENTED_EDGE('',*,*,#9975,.T.);
#13179=ORIENTED_EDGE('',*,*,#9980,.T.);
#13180=ORIENTED_EDGE('',*,*,#9981,.F.);
#13181=ORIENTED_EDGE('',*,*,#9982,.T.);
#13182=ORIENTED_EDGE('',*,*,#9978,.T.);
#13183=ORIENTED_EDGE('',*,*,#9983,.T.);
#13184=ORIENTED_EDGE('',*,*,#9984,.F.);
#13185=ORIENTED_EDGE('',*,*,#9985,.T.);
#13186=ORIENTED_EDGE('',*,*,#9981,.T.);
#13187=ORIENTED_EDGE('',*,*,#9986,.F.);
#13188=ORIENTED_EDGE('',*,*,#9987,.F.);
#13189=ORIENTED_EDGE('',*,*,#9988,.T.);
#13190=ORIENTED_EDGE('',*,*,#9989,.T.);
#13191=ORIENTED_EDGE('',*,*,#9990,.F.);
#13192=ORIENTED_EDGE('',*,*,#9991,.F.);
#13193=ORIENTED_EDGE('',*,*,#9992,.T.);
#13194=ORIENTED_EDGE('',*,*,#9987,.T.);
#13195=ORIENTED_EDGE('',*,*,#9993,.F.);
#13196=ORIENTED_EDGE('',*,*,#9994,.F.);
#13197=ORIENTED_EDGE('',*,*,#9995,.T.);
#13198=ORIENTED_EDGE('',*,*,#9991,.T.);
#13199=ORIENTED_EDGE('',*,*,#9996,.T.);
#13200=ORIENTED_EDGE('',*,*,#9997,.F.);
#13201=ORIENTED_EDGE('',*,*,#9998,.T.);
#13202=ORIENTED_EDGE('',*,*,#9994,.T.);
#13203=ORIENTED_EDGE('',*,*,#9999,.T.);
#13204=ORIENTED_EDGE('',*,*,#10000,.F.);
#13205=ORIENTED_EDGE('',*,*,#10001,.T.);
#13206=ORIENTED_EDGE('',*,*,#9997,.T.);
#13207=ORIENTED_EDGE('',*,*,#10002,.T.);
#13208=ORIENTED_EDGE('',*,*,#10003,.F.);
#13209=ORIENTED_EDGE('',*,*,#10004,.T.);
#13210=ORIENTED_EDGE('',*,*,#10000,.T.);
#13211=ORIENTED_EDGE('',*,*,#10005,.T.);
#13212=ORIENTED_EDGE('',*,*,#10006,.F.);
#13213=ORIENTED_EDGE('',*,*,#10007,.T.);
#13214=ORIENTED_EDGE('',*,*,#10003,.T.);
#13215=ORIENTED_EDGE('',*,*,#10008,.T.);
#13216=ORIENTED_EDGE('',*,*,#10009,.F.);
#13217=ORIENTED_EDGE('',*,*,#10010,.T.);
#13218=ORIENTED_EDGE('',*,*,#10006,.T.);
#13219=ORIENTED_EDGE('',*,*,#10011,.F.);
#13220=ORIENTED_EDGE('',*,*,#10012,.F.);
#13221=ORIENTED_EDGE('',*,*,#10013,.F.);
#13222=ORIENTED_EDGE('',*,*,#10014,.F.);
#13223=ORIENTED_EDGE('',*,*,#10015,.F.);
#13224=ORIENTED_EDGE('',*,*,#10016,.F.);
#13225=ORIENTED_EDGE('',*,*,#10017,.F.);
#13226=ORIENTED_EDGE('',*,*,#10018,.F.);
#13227=ORIENTED_EDGE('',*,*,#10019,.F.);
#13228=ORIENTED_EDGE('',*,*,#10020,.F.);
#13229=ORIENTED_EDGE('',*,*,#10021,.F.);
#13230=ORIENTED_EDGE('',*,*,#10022,.F.);
#13231=ORIENTED_EDGE('',*,*,#10023,.F.);
#13232=ORIENTED_EDGE('',*,*,#10024,.F.);
#13233=ORIENTED_EDGE('',*,*,#10025,.F.);
#13234=ORIENTED_EDGE('',*,*,#10026,.F.);
#13235=ORIENTED_EDGE('',*,*,#10027,.F.);
#13236=ORIENTED_EDGE('',*,*,#10028,.F.);
#13237=ORIENTED_EDGE('',*,*,#9963,.F.);
#13238=ORIENTED_EDGE('',*,*,#9967,.F.);
#13239=ORIENTED_EDGE('',*,*,#9970,.F.);
#13240=ORIENTED_EDGE('',*,*,#9973,.F.);
#13241=ORIENTED_EDGE('',*,*,#9976,.F.);
#13242=ORIENTED_EDGE('',*,*,#9979,.F.);
#13243=ORIENTED_EDGE('',*,*,#9982,.F.);
#13244=ORIENTED_EDGE('',*,*,#9985,.F.);
#13245=ORIENTED_EDGE('',*,*,#10029,.F.);
#13246=ORIENTED_EDGE('',*,*,#9988,.F.);
#13247=ORIENTED_EDGE('',*,*,#9992,.F.);
#13248=ORIENTED_EDGE('',*,*,#9995,.F.);
#13249=ORIENTED_EDGE('',*,*,#9998,.F.);
#13250=ORIENTED_EDGE('',*,*,#10001,.F.);
#13251=ORIENTED_EDGE('',*,*,#10004,.F.);
#13252=ORIENTED_EDGE('',*,*,#10007,.F.);
#13253=ORIENTED_EDGE('',*,*,#10010,.F.);
#13254=ORIENTED_EDGE('',*,*,#10030,.F.);
#13255=ORIENTED_EDGE('',*,*,#10031,.T.);
#13256=ORIENTED_EDGE('',*,*,#9989,.F.);
#13257=ORIENTED_EDGE('',*,*,#10029,.T.);
#13258=ORIENTED_EDGE('',*,*,#9984,.T.);
#13259=ORIENTED_EDGE('',*,*,#10032,.T.);
#13260=ORIENTED_EDGE('',*,*,#10033,.T.);
#13261=ORIENTED_EDGE('',*,*,#10030,.T.);
#13262=ORIENTED_EDGE('',*,*,#10009,.T.);
#13263=ORIENTED_EDGE('',*,*,#10034,.T.);
#13264=ORIENTED_EDGE('',*,*,#10035,.F.);
#13265=ORIENTED_EDGE('',*,*,#10011,.T.);
#13266=ORIENTED_EDGE('',*,*,#10033,.F.);
#13267=ORIENTED_EDGE('',*,*,#10036,.T.);
#13268=ORIENTED_EDGE('',*,*,#10037,.F.);
#13269=ORIENTED_EDGE('',*,*,#10012,.T.);
#13270=ORIENTED_EDGE('',*,*,#10035,.T.);
#13271=ORIENTED_EDGE('',*,*,#10038,.T.);
#13272=ORIENTED_EDGE('',*,*,#10039,.F.);
#13273=ORIENTED_EDGE('',*,*,#10013,.T.);
#13274=ORIENTED_EDGE('',*,*,#10037,.T.);
#13275=ORIENTED_EDGE('',*,*,#10040,.T.);
#13276=ORIENTED_EDGE('',*,*,#10041,.F.);
#13277=ORIENTED_EDGE('',*,*,#10014,.T.);
#13278=ORIENTED_EDGE('',*,*,#10039,.T.);
#13279=ORIENTED_EDGE('',*,*,#10042,.T.);
#13280=ORIENTED_EDGE('',*,*,#10043,.F.);
#13281=ORIENTED_EDGE('',*,*,#10015,.T.);
#13282=ORIENTED_EDGE('',*,*,#10041,.T.);
#13283=ORIENTED_EDGE('',*,*,#10044,.T.);
#13284=ORIENTED_EDGE('',*,*,#10045,.F.);
#13285=ORIENTED_EDGE('',*,*,#10016,.T.);
#13286=ORIENTED_EDGE('',*,*,#10043,.T.);
#13287=ORIENTED_EDGE('',*,*,#10046,.T.);
#13288=ORIENTED_EDGE('',*,*,#10047,.F.);
#13289=ORIENTED_EDGE('',*,*,#10017,.T.);
#13290=ORIENTED_EDGE('',*,*,#10045,.T.);
#13291=ORIENTED_EDGE('',*,*,#10048,.T.);
#13292=ORIENTED_EDGE('',*,*,#10049,.F.);
#13293=ORIENTED_EDGE('',*,*,#10018,.T.);
#13294=ORIENTED_EDGE('',*,*,#10047,.T.);
#13295=ORIENTED_EDGE('',*,*,#10050,.T.);
#13296=ORIENTED_EDGE('',*,*,#10051,.F.);
#13297=ORIENTED_EDGE('',*,*,#10019,.T.);
#13298=ORIENTED_EDGE('',*,*,#10049,.T.);
#13299=ORIENTED_EDGE('',*,*,#10052,.T.);
#13300=ORIENTED_EDGE('',*,*,#10053,.F.);
#13301=ORIENTED_EDGE('',*,*,#10020,.T.);
#13302=ORIENTED_EDGE('',*,*,#10051,.T.);
#13303=ORIENTED_EDGE('',*,*,#10054,.T.);
#13304=ORIENTED_EDGE('',*,*,#10055,.F.);
#13305=ORIENTED_EDGE('',*,*,#10021,.T.);
#13306=ORIENTED_EDGE('',*,*,#10053,.T.);
#13307=ORIENTED_EDGE('',*,*,#10056,.T.);
#13308=ORIENTED_EDGE('',*,*,#10057,.F.);
#13309=ORIENTED_EDGE('',*,*,#10022,.T.);
#13310=ORIENTED_EDGE('',*,*,#10055,.T.);
#13311=ORIENTED_EDGE('',*,*,#10058,.T.);
#13312=ORIENTED_EDGE('',*,*,#10059,.F.);
#13313=ORIENTED_EDGE('',*,*,#10023,.T.);
#13314=ORIENTED_EDGE('',*,*,#10057,.T.);
#13315=ORIENTED_EDGE('',*,*,#10060,.T.);
#13316=ORIENTED_EDGE('',*,*,#10061,.F.);
#13317=ORIENTED_EDGE('',*,*,#10024,.T.);
#13318=ORIENTED_EDGE('',*,*,#10059,.T.);
#13319=ORIENTED_EDGE('',*,*,#10062,.T.);
#13320=ORIENTED_EDGE('',*,*,#10063,.F.);
#13321=ORIENTED_EDGE('',*,*,#10025,.T.);
#13322=ORIENTED_EDGE('',*,*,#10061,.T.);
#13323=ORIENTED_EDGE('',*,*,#10064,.T.);
#13324=ORIENTED_EDGE('',*,*,#10065,.F.);
#13325=ORIENTED_EDGE('',*,*,#10026,.T.);
#13326=ORIENTED_EDGE('',*,*,#10063,.T.);
#13327=ORIENTED_EDGE('',*,*,#10066,.T.);
#13328=ORIENTED_EDGE('',*,*,#10067,.F.);
#13329=ORIENTED_EDGE('',*,*,#10027,.T.);
#13330=ORIENTED_EDGE('',*,*,#10065,.T.);
#13331=ORIENTED_EDGE('',*,*,#10068,.T.);
#13332=ORIENTED_EDGE('',*,*,#9964,.F.);
#13333=ORIENTED_EDGE('',*,*,#10028,.T.);
#13334=ORIENTED_EDGE('',*,*,#10067,.T.);
#13335=ORIENTED_EDGE('',*,*,#10032,.F.);
#13336=ORIENTED_EDGE('',*,*,#10008,.F.);
#13337=ORIENTED_EDGE('',*,*,#10005,.F.);
#13338=ORIENTED_EDGE('',*,*,#10002,.F.);
#13339=ORIENTED_EDGE('',*,*,#9999,.F.);
#13340=ORIENTED_EDGE('',*,*,#9996,.F.);
#13341=ORIENTED_EDGE('',*,*,#9993,.T.);
#13342=ORIENTED_EDGE('',*,*,#9990,.T.);
#13343=ORIENTED_EDGE('',*,*,#9986,.T.);
#13344=ORIENTED_EDGE('',*,*,#10031,.F.);
#13345=ORIENTED_EDGE('',*,*,#9983,.F.);
#13346=ORIENTED_EDGE('',*,*,#9980,.F.);
#13347=ORIENTED_EDGE('',*,*,#9977,.F.);
#13348=ORIENTED_EDGE('',*,*,#9974,.F.);
#13349=ORIENTED_EDGE('',*,*,#9971,.F.);
#13350=ORIENTED_EDGE('',*,*,#9968,.F.);
#13351=ORIENTED_EDGE('',*,*,#9965,.F.);
#13352=ORIENTED_EDGE('',*,*,#9961,.F.);
#13353=ORIENTED_EDGE('',*,*,#10068,.F.);
#13354=ORIENTED_EDGE('',*,*,#10066,.F.);
#13355=ORIENTED_EDGE('',*,*,#10064,.F.);
#13356=ORIENTED_EDGE('',*,*,#10062,.F.);
#13357=ORIENTED_EDGE('',*,*,#10060,.F.);
#13358=ORIENTED_EDGE('',*,*,#10058,.F.);
#13359=ORIENTED_EDGE('',*,*,#10056,.F.);
#13360=ORIENTED_EDGE('',*,*,#10054,.F.);
#13361=ORIENTED_EDGE('',*,*,#10052,.F.);
#13362=ORIENTED_EDGE('',*,*,#10050,.F.);
#13363=ORIENTED_EDGE('',*,*,#10048,.F.);
#13364=ORIENTED_EDGE('',*,*,#10046,.F.);
#13365=ORIENTED_EDGE('',*,*,#10044,.F.);
#13366=ORIENTED_EDGE('',*,*,#10042,.F.);
#13367=ORIENTED_EDGE('',*,*,#10040,.F.);
#13368=ORIENTED_EDGE('',*,*,#10038,.F.);
#13369=ORIENTED_EDGE('',*,*,#10036,.F.);
#13370=ORIENTED_EDGE('',*,*,#10034,.F.);
#18535=PLANE('',#20258);
#18536=PLANE('',#20275);
#18537=PLANE('',#20282);
#18538=PLANE('',#20289);
#18539=PLANE('',#20292);
#18540=PLANE('',#20295);
#18541=PLANE('',#20296);
#18542=PLANE('',#20297);
#18543=PLANE('',#20298);
#18544=PLANE('',#20299);
#18545=PLANE('',#20300);
#18546=PLANE('',#20301);
#18547=PLANE('',#20302);
#18548=PLANE('',#20305);
#18549=PLANE('',#20306);
#18550=PLANE('',#20307);
#18551=PLANE('',#20308);
#18552=PLANE('',#20309);
#18553=PLANE('',#20310);
#18554=PLANE('',#20317);
#18555=PLANE('',#20324);
#18556=PLANE('',#20327);
#18557=PLANE('',#20328);
#18558=PLANE('',#20338);
#18559=PLANE('',#20345);
#18560=PLANE('',#20359);
#18561=PLANE('',#20360);
#18562=PLANE('',#20361);
#18563=PLANE('',#20362);
#18564=PLANE('',#20367);
#18565=PLANE('',#20368);
#18566=PLANE('',#20381);
#18567=PLANE('',#20382);
#18568=PLANE('',#20383);
#18569=PLANE('',#20384);
#18570=PLANE('',#20396);
#18571=PLANE('',#20397);
#18572=PLANE('',#20398);
#18573=PLANE('',#20399);
#18574=PLANE('',#20401);
#18575=PLANE('',#20403);
#18576=PLANE('',#20405);
#18577=PLANE('',#20406);
#18578=PLANE('',#20407);
#18579=PLANE('',#20408);
#18580=PLANE('',#20410);
#18581=PLANE('',#20412);
#18582=PLANE('',#20416);
#18583=PLANE('',#20420);
#18584=PLANE('',#20421);
#18585=PLANE('',#20425);
#18586=PLANE('',#20429);
#18587=PLANE('',#20433);
#18588=PLANE('',#20434);
#18589=PLANE('',#20435);
#18590=PLANE('',#20436);
#18591=PLANE('',#20437);
#18592=PLANE('',#20438);
#18593=PLANE('',#20439);
#18594=PLANE('',#20440);
#18595=PLANE('',#20441);
#18596=PLANE('',#20442);
#18597=PLANE('',#20446);
#18598=PLANE('',#20459);
#18599=PLANE('',#20460);
#18600=PLANE('',#20463);
#18601=PLANE('',#20470);
#18602=PLANE('',#20477);
#18603=PLANE('',#20478);
#18604=PLANE('',#20479);
#18605=PLANE('',#20486);
#18606=PLANE('',#20491);
#19064=ADVANCED_FACE('',(#1207),#18535,.T.);
#19065=ADVANCED_FACE('',(#1208),#18536,.F.);
#19066=ADVANCED_FACE('',(#1209),#781,.F.);
#19067=ADVANCED_FACE('',(#1210),#782,.T.);
#19068=ADVANCED_FACE('',(#1211),#783,.F.);
#19069=ADVANCED_FACE('',(#1212),#18537,.F.);
#19070=ADVANCED_FACE('',(#1213),#784,.F.);
#19071=ADVANCED_FACE('',(#1214),#785,.T.);
#19072=ADVANCED_FACE('',(#1215),#786,.F.);
#19073=ADVANCED_FACE('',(#1216),#18538,.F.);
#19074=ADVANCED_FACE('',(#1217),#787,.T.);
#19075=ADVANCED_FACE('',(#1218),#18539,.F.);
#19076=ADVANCED_FACE('',(#1219),#788,.T.);
#19077=ADVANCED_FACE('',(#1220),#18540,.F.);
#19078=ADVANCED_FACE('',(#1221),#18541,.F.);
#19079=ADVANCED_FACE('',(#1222),#18542,.F.);
#19080=ADVANCED_FACE('',(#1223),#18543,.F.);
#19081=ADVANCED_FACE('',(#1224),#18544,.F.);
#19082=ADVANCED_FACE('',(#1225),#18545,.F.);
#19083=ADVANCED_FACE('',(#1226),#18546,.F.);
#19084=ADVANCED_FACE('',(#1227),#18547,.F.);
#19085=ADVANCED_FACE('',(#1228),#789,.T.);
#19086=ADVANCED_FACE('',(#1229),#18548,.F.);
#19087=ADVANCED_FACE('',(#1230),#18549,.F.);
#19088=ADVANCED_FACE('',(#1231),#18550,.F.);
#19089=ADVANCED_FACE('',(#1232),#18551,.F.);
#19090=ADVANCED_FACE('',(#1233),#18552,.F.);
#19091=ADVANCED_FACE('',(#1234),#18553,.F.);
#19092=ADVANCED_FACE('',(#1235),#790,.F.);
#19093=ADVANCED_FACE('',(#1236),#791,.T.);
#19094=ADVANCED_FACE('',(#1237),#792,.F.);
#19095=ADVANCED_FACE('',(#1238),#18554,.F.);
#19096=ADVANCED_FACE('',(#1239),#793,.F.);
#19097=ADVANCED_FACE('',(#1240),#794,.T.);
#19098=ADVANCED_FACE('',(#1241),#795,.F.);
#19099=ADVANCED_FACE('',(#1242),#18555,.F.);
#19100=ADVANCED_FACE('',(#1243),#796,.T.);
#19101=ADVANCED_FACE('',(#1244),#18556,.F.);
#19102=ADVANCED_FACE('',(#1245),#18557,.F.);
#19103=ADVANCED_FACE('',(#1246),#797,.F.);
#19104=ADVANCED_FACE('',(#1247),#798,.T.);
#19105=ADVANCED_FACE('',(#1248),#799,.F.);
#19106=ADVANCED_FACE('',(#1249),#18558,.F.);
#19107=ADVANCED_FACE('',(#1250),#800,.F.);
#19108=ADVANCED_FACE('',(#1251),#801,.T.);
#19109=ADVANCED_FACE('',(#1252),#18559,.F.);
#19110=ADVANCED_FACE('',(#1253),#18560,.F.);
#19111=ADVANCED_FACE('',(#1254),#18561,.F.);
#19112=ADVANCED_FACE('',(#1255),#18562,.F.);
#19113=ADVANCED_FACE('',(#1256,#635,#636),#18563,.F.);
#19114=ADVANCED_FACE('',(#1257),#802,.F.);
#19115=ADVANCED_FACE('',(#1258),#18564,.F.);
#19116=ADVANCED_FACE('',(#1259),#18565,.T.);
#19117=ADVANCED_FACE('',(#1260),#18566,.T.);
#19118=ADVANCED_FACE('',(#1261),#18567,.T.);
#19119=ADVANCED_FACE('',(#1262),#18568,.T.);
#19120=ADVANCED_FACE('',(#1263,#637,#638),#18569,.T.);
#19121=ADVANCED_FACE('',(#1264),#803,.F.);
#19122=ADVANCED_FACE('',(#1265),#804,.F.);
#19123=ADVANCED_FACE('',(#1266),#805,.F.);
#19124=ADVANCED_FACE('',(#1267),#806,.F.);
#19125=ADVANCED_FACE('',(#1268),#807,.F.);
#19126=ADVANCED_FACE('',(#1269),#18570,.F.);
#19127=ADVANCED_FACE('',(#1270),#18571,.F.);
#19128=ADVANCED_FACE('',(#1271,#639,#640),#18572,.F.);
#19129=ADVANCED_FACE('',(#1272),#18573,.F.);
#19130=ADVANCED_FACE('',(#1273),#808,.T.);
#19131=ADVANCED_FACE('',(#1274),#18574,.F.);
#19132=ADVANCED_FACE('',(#1275),#809,.T.);
#19133=ADVANCED_FACE('',(#1276),#18575,.F.);
#19134=ADVANCED_FACE('',(#1277),#810,.F.);
#19135=ADVANCED_FACE('',(#1278),#18576,.F.);
#19136=ADVANCED_FACE('',(#1279),#18577,.F.);
#19137=ADVANCED_FACE('',(#1280,#641,#642),#18578,.F.);
#19138=ADVANCED_FACE('',(#1281),#18579,.F.);
#19139=ADVANCED_FACE('',(#1282),#811,.T.);
#19140=ADVANCED_FACE('',(#1283),#18580,.F.);
#19141=ADVANCED_FACE('',(#1284),#812,.T.);
#19142=ADVANCED_FACE('',(#1285),#18581,.F.);
#19143=ADVANCED_FACE('',(#1286),#813,.F.);
#19144=ADVANCED_FACE('',(#1287),#814,.T.);
#19145=ADVANCED_FACE('',(#1288),#815,.F.);
#19146=ADVANCED_FACE('',(#1289),#18582,.F.);
#19147=ADVANCED_FACE('',(#1290),#816,.F.);
#19148=ADVANCED_FACE('',(#1291),#817,.T.);
#19149=ADVANCED_FACE('',(#1292),#818,.F.);
#19150=ADVANCED_FACE('',(#1293),#18583,.F.);
#19151=ADVANCED_FACE('',(#1294),#18584,.F.);
#19152=ADVANCED_FACE('',(#1295),#819,.F.);
#19153=ADVANCED_FACE('',(#1296),#18585,.F.);
#19154=ADVANCED_FACE('',(#1297),#820,.T.);
#19155=ADVANCED_FACE('',(#1298),#18586,.F.);
#19156=ADVANCED_FACE('',(#1299),#821,.T.);
#19157=ADVANCED_FACE('',(#1300),#18587,.F.);
#19158=ADVANCED_FACE('',(#1301),#18588,.F.);
#19159=ADVANCED_FACE('',(#1302),#18589,.F.);
#19160=ADVANCED_FACE('',(#1303),#18590,.F.);
#19161=ADVANCED_FACE('',(#1304),#18591,.F.);
#19162=ADVANCED_FACE('',(#1305),#18592,.F.);
#19163=ADVANCED_FACE('',(#1306),#18593,.F.);
#19164=ADVANCED_FACE('',(#1307),#18594,.F.);
#19165=ADVANCED_FACE('',(#1308),#18595,.F.);
#19166=ADVANCED_FACE('',(#1309),#18596,.F.);
#19167=ADVANCED_FACE('',(#1310),#822,.T.);
#19168=ADVANCED_FACE('',(#1311),#18597,.T.);
#19169=ADVANCED_FACE('',(#1312),#18598,.F.);
#19170=ADVANCED_FACE('',(#1313),#18599,.F.);
#19171=ADVANCED_FACE('',(#1314),#823,.T.);
#19172=ADVANCED_FACE('',(#1315),#18600,.F.);
#19173=ADVANCED_FACE('',(#1316),#824,.F.);
#19174=ADVANCED_FACE('',(#1317),#825,.T.);
#19175=ADVANCED_FACE('',(#1318),#826,.F.);
#19176=ADVANCED_FACE('',(#1319),#18601,.F.);
#19177=ADVANCED_FACE('',(#1320),#827,.F.);
#19178=ADVANCED_FACE('',(#1321),#828,.T.);
#19179=ADVANCED_FACE('',(#1322),#829,.F.);
#19180=ADVANCED_FACE('',(#1323),#18602,.F.);
#19181=ADVANCED_FACE('',(#1324),#18603,.F.);
#19182=ADVANCED_FACE('',(#1325),#18604,.F.);
#19183=ADVANCED_FACE('',(#1326),#830,.F.);
#19184=ADVANCED_FACE('',(#1327),#831,.T.);
#19185=ADVANCED_FACE('',(#1328),#832,.F.);
#19186=ADVANCED_FACE('',(#1329),#18605,.F.);
#19187=ADVANCED_FACE('',(#1330),#833,.F.);
#19188=ADVANCED_FACE('',(#1331),#834,.T.);
#19189=ADVANCED_FACE('',(#1332),#18606,.F.);
#20108=CLOSED_SHELL('',(#19064,#19065,#19066,#19067,#19068,#19069,#19070,
#19071,#19072,#19073,#19074,#19075,#19076,#19077,#19078,#19079,#19080,#19081,
#19082,#19083,#19084,#19085,#19086,#19087,#19088,#19089,#19090,#19091,#19092,
#19093,#19094,#19095,#19096,#19097,#19098,#19099,#19100,#19101));
#20109=CLOSED_SHELL('',(#19102,#19103,#19104,#19105,#19106,#19107,#19108,
#19109,#19110,#19111,#19112,#19113,#19114,#19115,#19116,#19117,#19118,#19119,
#19120,#19121,#19122,#19123,#19124,#19125,#19126,#19127,#19128,#19129,#19130,
#19131,#19132,#19133,#19134,#19135,#19136,#19137,#19138,#19139,#19140,#19141,
#19142,#19143,#19144,#19145,#19146,#19147,#19148,#19149,#19150,#19151));
#20110=CLOSED_SHELL('',(#19152,#19153,#19154,#19155,#19156,#19157,#19158,
#19159,#19160,#19161,#19162,#19163,#19164,#19165,#19166,#19167,#19168,#19169,
#19170,#19171,#19172,#19173,#19174,#19175,#19176,#19177,#19178,#19179,#19180,
#19181,#19182,#19183,#19184,#19185,#19186,#19187,#19188,#19189));
#20257=AXIS2_PLACEMENT_3D('',#27148,#21928,#21929);
#20258=AXIS2_PLACEMENT_3D('',#27149,#21930,#21931);
#20259=AXIS2_PLACEMENT_3D('',#27160,#21936,#21937);
#20260=AXIS2_PLACEMENT_3D('',#27164,#21939,#21940);
#20261=AXIS2_PLACEMENT_3D('',#27168,#21942,#21943);
#20262=AXIS2_PLACEMENT_3D('',#27170,#21944,#21945);
#20263=AXIS2_PLACEMENT_3D('',#27172,#21946,#21947);
#20264=AXIS2_PLACEMENT_3D('',#27176,#21949,#21950);
#20265=AXIS2_PLACEMENT_3D('',#27178,#21951,#21952);
#20266=AXIS2_PLACEMENT_3D('',#27180,#21953,#21954);
#20267=AXIS2_PLACEMENT_3D('',#27188,#21958,#21959);
#20268=AXIS2_PLACEMENT_3D('',#27190,#21960,#21961);
#20269=AXIS2_PLACEMENT_3D('',#27192,#21962,#21963);
#20270=AXIS2_PLACEMENT_3D('',#27196,#21965,#21966);
#20271=AXIS2_PLACEMENT_3D('',#27198,#21967,#21968);
#20272=AXIS2_PLACEMENT_3D('',#27200,#21969,#21970);
#20273=AXIS2_PLACEMENT_3D('',#27204,#21972,#21973);
#20274=AXIS2_PLACEMENT_3D('',#27208,#21975,#21976);
#20275=AXIS2_PLACEMENT_3D('',#27222,#21984,#21985);
#20276=AXIS2_PLACEMENT_3D('',#27228,#21989,#21990);
#20277=AXIS2_PLACEMENT_3D('',#27230,#21991,#21992);
#20278=AXIS2_PLACEMENT_3D('',#27232,#21994,#21995);
#20279=AXIS2_PLACEMENT_3D('',#27234,#21996,#21997);
#20280=AXIS2_PLACEMENT_3D('',#27236,#21999,#22000);
#20281=AXIS2_PLACEMENT_3D('',#27238,#22001,#22002);
#20282=AXIS2_PLACEMENT_3D('',#27240,#22004,#22005);
#20283=AXIS2_PLACEMENT_3D('',#27244,#22008,#22009);
#20284=AXIS2_PLACEMENT_3D('',#27246,#22010,#22011);
#20285=AXIS2_PLACEMENT_3D('',#27248,#22013,#22014);
#20286=AXIS2_PLACEMENT_3D('',#27250,#22015,#22016);
#20287=AXIS2_PLACEMENT_3D('',#27252,#22018,#22019);
#20288=AXIS2_PLACEMENT_3D('',#27254,#22020,#22021);
#20289=AXIS2_PLACEMENT_3D('',#27256,#22023,#22024);
#20290=AXIS2_PLACEMENT_3D('',#27260,#22027,#22028);
#20291=AXIS2_PLACEMENT_3D('',#27262,#22029,#22030);
#20292=AXIS2_PLACEMENT_3D('',#27264,#22032,#22033);
#20293=AXIS2_PLACEMENT_3D('',#27268,#22036,#22037);
#20294=AXIS2_PLACEMENT_3D('',#27270,#22038,#22039);
#20295=AXIS2_PLACEMENT_3D('',#27272,#22041,#22042);
#20296=AXIS2_PLACEMENT_3D('',#27276,#22045,#22046);
#20297=AXIS2_PLACEMENT_3D('',#27280,#22049,#22050);
#20298=AXIS2_PLACEMENT_3D('',#27284,#22053,#22054);
#20299=AXIS2_PLACEMENT_3D('',#27288,#22057,#22058);
#20300=AXIS2_PLACEMENT_3D('',#27294,#22062,#22063);
#20301=AXIS2_PLACEMENT_3D('',#27298,#22066,#22067);
#20302=AXIS2_PLACEMENT_3D('',#27302,#22070,#22071);
#20303=AXIS2_PLACEMENT_3D('',#27306,#22074,#22075);
#20304=AXIS2_PLACEMENT_3D('',#27308,#22076,#22077);
#20305=AXIS2_PLACEMENT_3D('',#27310,#22079,#22080);
#20306=AXIS2_PLACEMENT_3D('',#27314,#22083,#22084);
#20307=AXIS2_PLACEMENT_3D('',#27318,#22087,#22088);
#20308=AXIS2_PLACEMENT_3D('',#27320,#22090,#22091);
#20309=AXIS2_PLACEMENT_3D('',#27324,#22094,#22095);
#20310=AXIS2_PLACEMENT_3D('',#27328,#22098,#22099);
#20311=AXIS2_PLACEMENT_3D('',#27332,#22102,#22103);
#20312=AXIS2_PLACEMENT_3D('',#27335,#22105,#22106);
#20313=AXIS2_PLACEMENT_3D('',#27336,#22107,#22108);
#20314=AXIS2_PLACEMENT_3D('',#27339,#22110,#22111);
#20315=AXIS2_PLACEMENT_3D('',#27340,#22112,#22113);
#20316=AXIS2_PLACEMENT_3D('',#27343,#22115,#22116);
#20317=AXIS2_PLACEMENT_3D('',#27344,#22117,#22118);
#20318=AXIS2_PLACEMENT_3D('',#27348,#22121,#22122);
#20319=AXIS2_PLACEMENT_3D('',#27351,#22124,#22125);
#20320=AXIS2_PLACEMENT_3D('',#27352,#22126,#22127);
#20321=AXIS2_PLACEMENT_3D('',#27355,#22129,#22130);
#20322=AXIS2_PLACEMENT_3D('',#27356,#22131,#22132);
#20323=AXIS2_PLACEMENT_3D('',#27359,#22134,#22135);
#20324=AXIS2_PLACEMENT_3D('',#27360,#22136,#22137);
#20325=AXIS2_PLACEMENT_3D('',#27364,#22140,#22141);
#20326=AXIS2_PLACEMENT_3D('',#27365,#22142,#22143);
#20327=AXIS2_PLACEMENT_3D('',#27366,#22144,#22145);
#20328=AXIS2_PLACEMENT_3D('',#27367,#22146,#22147);
#20329=AXIS2_PLACEMENT_3D('',#27376,#22152,#22153);
#20330=AXIS2_PLACEMENT_3D('',#27378,#22154,#22155);
#20331=AXIS2_PLACEMENT_3D('',#27381,#22157,#22158);
#20332=AXIS2_PLACEMENT_3D('',#27382,#22159,#22160);
#20333=AXIS2_PLACEMENT_3D('',#27384,#22161,#22162);
#20334=AXIS2_PLACEMENT_3D('',#27387,#22164,#22165);
#20335=AXIS2_PLACEMENT_3D('',#27388,#22166,#22167);
#20336=AXIS2_PLACEMENT_3D('',#27390,#22168,#22169);
#20337=AXIS2_PLACEMENT_3D('',#27393,#22171,#22172);
#20338=AXIS2_PLACEMENT_3D('',#27394,#22173,#22174);
#20339=AXIS2_PLACEMENT_3D('',#27400,#22178,#22179);
#20340=AXIS2_PLACEMENT_3D('',#27402,#22180,#22181);
#20341=AXIS2_PLACEMENT_3D('',#27405,#22183,#22184);
#20342=AXIS2_PLACEMENT_3D('',#27406,#22185,#22186);
#20343=AXIS2_PLACEMENT_3D('',#27408,#22187,#22188);
#20344=AXIS2_PLACEMENT_3D('',#27411,#22190,#22191);
#20345=AXIS2_PLACEMENT_3D('',#27412,#22192,#22193);
#20346=AXIS2_PLACEMENT_3D('',#27425,#22199,#22200);
#20347=AXIS2_PLACEMENT_3D('',#27429,#22202,#22203);
#20348=AXIS2_PLACEMENT_3D('',#27432,#22205,#22206);
#20349=AXIS2_PLACEMENT_3D('',#27438,#22209,#22210);
#20350=AXIS2_PLACEMENT_3D('',#27440,#22211,#22212);
#20351=AXIS2_PLACEMENT_3D('',#27442,#22213,#22214);
#20352=AXIS2_PLACEMENT_3D('',#27446,#22216,#22217);
#20353=AXIS2_PLACEMENT_3D('',#27448,#22218,#22219);
#20354=AXIS2_PLACEMENT_3D('',#27450,#22220,#22221);
#20355=AXIS2_PLACEMENT_3D('',#27454,#22223,#22224);
#20356=AXIS2_PLACEMENT_3D('',#27458,#22226,#22227);
#20357=AXIS2_PLACEMENT_3D('',#27476,#22236,#22237);
#20358=AXIS2_PLACEMENT_3D('',#27480,#22239,#22240);
#20359=AXIS2_PLACEMENT_3D('',#27486,#22244,#22245);
#20360=AXIS2_PLACEMENT_3D('',#27492,#22249,#22250);
#20361=AXIS2_PLACEMENT_3D('',#27496,#22253,#22254);
#20362=AXIS2_PLACEMENT_3D('',#27500,#22257,#22258);
#20363=AXIS2_PLACEMENT_3D('',#27505,#22261,#22262);
#20364=AXIS2_PLACEMENT_3D('',#27507,#22263,#22264);
#20365=AXIS2_PLACEMENT_3D('',#27508,#22265,#22266);
#20366=AXIS2_PLACEMENT_3D('',#27511,#22268,#22269);
#20367=AXIS2_PLACEMENT_3D('',#27512,#22270,#22271);
#20368=AXIS2_PLACEMENT_3D('',#27516,#22274,#22275);
#20369=AXIS2_PLACEMENT_3D('',#27518,#22276,#22277);
#20370=AXIS2_PLACEMENT_3D('',#27536,#22286,#22287);
#20371=AXIS2_PLACEMENT_3D('',#27540,#22289,#22290);
#20372=AXIS2_PLACEMENT_3D('',#27544,#22292,#22293);
#20373=AXIS2_PLACEMENT_3D('',#27546,#22294,#22295);
#20374=AXIS2_PLACEMENT_3D('',#27548,#22296,#22297);
#20375=AXIS2_PLACEMENT_3D('',#27552,#22299,#22300);
#20376=AXIS2_PLACEMENT_3D('',#27554,#22301,#22302);
#20377=AXIS2_PLACEMENT_3D('',#27556,#22303,#22304);
#20378=AXIS2_PLACEMENT_3D('',#27561,#22307,#22308);
#20379=AXIS2_PLACEMENT_3D('',#27565,#22310,#22311);
#20380=AXIS2_PLACEMENT_3D('',#27569,#22313,#22314);
#20381=AXIS2_PLACEMENT_3D('',#27577,#22319,#22320);
#20382=AXIS2_PLACEMENT_3D('',#27580,#22323,#22324);
#20383=AXIS2_PLACEMENT_3D('',#27582,#22326,#22327);
#20384=AXIS2_PLACEMENT_3D('',#27584,#22329,#22330);
#20385=AXIS2_PLACEMENT_3D('',#27587,#22332,#22333);
#20386=AXIS2_PLACEMENT_3D('',#27589,#22334,#22335);
#20387=AXIS2_PLACEMENT_3D('',#27590,#22336,#22337);
#20388=AXIS2_PLACEMENT_3D('',#27591,#22338,#22339);
#20389=AXIS2_PLACEMENT_3D('',#27594,#22341,#22342);
#20390=AXIS2_PLACEMENT_3D('',#27595,#22343,#22344);
#20391=AXIS2_PLACEMENT_3D('',#27598,#22346,#22347);
#20392=AXIS2_PLACEMENT_3D('',#27599,#22348,#22349);
#20393=AXIS2_PLACEMENT_3D('',#27602,#22351,#22352);
#20394=AXIS2_PLACEMENT_3D('',#27603,#22353,#22354);
#20395=AXIS2_PLACEMENT_3D('',#27606,#22356,#22357);
#20396=AXIS2_PLACEMENT_3D('',#27607,#22358,#22359);
#20397=AXIS2_PLACEMENT_3D('',#27609,#22361,#22362);
#20398=AXIS2_PLACEMENT_3D('',#27611,#22364,#22365);
#20399=AXIS2_PLACEMENT_3D('',#27613,#22367,#22368);
#20400=AXIS2_PLACEMENT_3D('',#27615,#22370,#22371);
#20401=AXIS2_PLACEMENT_3D('',#27617,#22373,#22374);
#20402=AXIS2_PLACEMENT_3D('',#27619,#22376,#22377);
#20403=AXIS2_PLACEMENT_3D('',#27621,#22379,#22380);
#20404=AXIS2_PLACEMENT_3D('',#27623,#22382,#22383);
#20405=AXIS2_PLACEMENT_3D('',#27624,#22384,#22385);
#20406=AXIS2_PLACEMENT_3D('',#27626,#22387,#22388);
#20407=AXIS2_PLACEMENT_3D('',#27628,#22390,#22391);
#20408=AXIS2_PLACEMENT_3D('',#27630,#22393,#22394);
#20409=AXIS2_PLACEMENT_3D('',#27632,#22396,#22397);
#20410=AXIS2_PLACEMENT_3D('',#27634,#22399,#22400);
#20411=AXIS2_PLACEMENT_3D('',#27636,#22402,#22403);
#20412=AXIS2_PLACEMENT_3D('',#27638,#22405,#22406);
#20413=AXIS2_PLACEMENT_3D('',#27640,#22408,#22409);
#20414=AXIS2_PLACEMENT_3D('',#27642,#22411,#22412);
#20415=AXIS2_PLACEMENT_3D('',#27644,#22414,#22415);
#20416=AXIS2_PLACEMENT_3D('',#27646,#22417,#22418);
#20417=AXIS2_PLACEMENT_3D('',#27648,#22420,#22421);
#20418=AXIS2_PLACEMENT_3D('',#27650,#22423,#22424);
#20419=AXIS2_PLACEMENT_3D('',#27652,#22426,#22427);
#20420=AXIS2_PLACEMENT_3D('',#27654,#22429,#22430);
#20421=AXIS2_PLACEMENT_3D('',#27656,#22432,#22433);
#20422=AXIS2_PLACEMENT_3D('',#27657,#22434,#22435);
#20423=AXIS2_PLACEMENT_3D('',#27660,#22436,#22437);
#20424=AXIS2_PLACEMENT_3D('',#27664,#22439,#22440);
#20425=AXIS2_PLACEMENT_3D('',#27666,#22442,#22443);
#20426=AXIS2_PLACEMENT_3D('',#27672,#22447,#22448);
#20427=AXIS2_PLACEMENT_3D('',#27674,#22449,#22450);
#20428=AXIS2_PLACEMENT_3D('',#27677,#22452,#22453);
#20429=AXIS2_PLACEMENT_3D('',#27678,#22454,#22455);
#20430=AXIS2_PLACEMENT_3D('',#27684,#22459,#22460);
#20431=AXIS2_PLACEMENT_3D('',#27686,#22461,#22462);
#20432=AXIS2_PLACEMENT_3D('',#27689,#22464,#22465);
#20433=AXIS2_PLACEMENT_3D('',#27690,#22466,#22467);
#20434=AXIS2_PLACEMENT_3D('',#27696,#22471,#22472);
#20435=AXIS2_PLACEMENT_3D('',#27702,#22476,#22477);
#20436=AXIS2_PLACEMENT_3D('',#27708,#22481,#22482);
#20437=AXIS2_PLACEMENT_3D('',#27717,#22487,#22488);
#20438=AXIS2_PLACEMENT_3D('',#27723,#22492,#22493);
#20439=AXIS2_PLACEMENT_3D('',#27729,#22497,#22498);
#20440=AXIS2_PLACEMENT_3D('',#27735,#22502,#22503);
#20441=AXIS2_PLACEMENT_3D('',#27741,#22507,#22508);
#20442=AXIS2_PLACEMENT_3D('',#27747,#22512,#22513);
#20443=AXIS2_PLACEMENT_3D('',#27753,#22517,#22518);
#20444=AXIS2_PLACEMENT_3D('',#27755,#22519,#22520);
#20445=AXIS2_PLACEMENT_3D('',#27758,#22522,#22523);
#20446=AXIS2_PLACEMENT_3D('',#27759,#22524,#22525);
#20447=AXIS2_PLACEMENT_3D('',#27762,#22526,#22527);
#20448=AXIS2_PLACEMENT_3D('',#27766,#22529,#22530);
#20449=AXIS2_PLACEMENT_3D('',#27768,#22531,#22532);
#20450=AXIS2_PLACEMENT_3D('',#27770,#22533,#22534);
#20451=AXIS2_PLACEMENT_3D('',#27774,#22536,#22537);
#20452=AXIS2_PLACEMENT_3D('',#27776,#22538,#22539);
#20453=AXIS2_PLACEMENT_3D('',#27778,#22540,#22541);
#20454=AXIS2_PLACEMENT_3D('',#27786,#22545,#22546);
#20455=AXIS2_PLACEMENT_3D('',#27788,#22547,#22548);
#20456=AXIS2_PLACEMENT_3D('',#27790,#22549,#22550);
#20457=AXIS2_PLACEMENT_3D('',#27794,#22552,#22553);
#20458=AXIS2_PLACEMENT_3D('',#27795,#22554,#22555);
#20459=AXIS2_PLACEMENT_3D('',#27798,#22558,#22559);
#20460=AXIS2_PLACEMENT_3D('',#27800,#22561,#22562);
#20461=AXIS2_PLACEMENT_3D('',#27804,#22565,#22566);
#20462=AXIS2_PLACEMENT_3D('',#27806,#22567,#22568);
#20463=AXIS2_PLACEMENT_3D('',#27808,#22570,#22571);
#20464=AXIS2_PLACEMENT_3D('',#27812,#22574,#22575);
#20465=AXIS2_PLACEMENT_3D('',#27814,#22576,#22577);
#20466=AXIS2_PLACEMENT_3D('',#27816,#22579,#22580);
#20467=AXIS2_PLACEMENT_3D('',#27818,#22581,#22582);
#20468=AXIS2_PLACEMENT_3D('',#27820,#22584,#22585);
#20469=AXIS2_PLACEMENT_3D('',#27822,#22586,#22587);
#20470=AXIS2_PLACEMENT_3D('',#27824,#22589,#22590);
#20471=AXIS2_PLACEMENT_3D('',#27828,#22593,#22594);
#20472=AXIS2_PLACEMENT_3D('',#27830,#22595,#22596);
#20473=AXIS2_PLACEMENT_3D('',#27832,#22598,#22599);
#20474=AXIS2_PLACEMENT_3D('',#27834,#22600,#22601);
#20475=AXIS2_PLACEMENT_3D('',#27836,#22603,#22604);
#20476=AXIS2_PLACEMENT_3D('',#27838,#22605,#22606);
#20477=AXIS2_PLACEMENT_3D('',#27840,#22608,#22609);
#20478=AXIS2_PLACEMENT_3D('',#27844,#22612,#22613);
#20479=AXIS2_PLACEMENT_3D('',#27848,#22616,#22617);
#20480=AXIS2_PLACEMENT_3D('',#27852,#22620,#22621);
#20481=AXIS2_PLACEMENT_3D('',#27854,#22622,#22623);
#20482=AXIS2_PLACEMENT_3D('',#27856,#22625,#22626);
#20483=AXIS2_PLACEMENT_3D('',#27858,#22627,#22628);
#20484=AXIS2_PLACEMENT_3D('',#27860,#22630,#22631);
#20485=AXIS2_PLACEMENT_3D('',#27862,#22632,#22633);
#20486=AXIS2_PLACEMENT_3D('',#27864,#22635,#22636);
#20487=AXIS2_PLACEMENT_3D('',#27868,#22639,#22640);
#20488=AXIS2_PLACEMENT_3D('',#27870,#22641,#22642);
#20489=AXIS2_PLACEMENT_3D('',#27872,#22644,#22645);
#20490=AXIS2_PLACEMENT_3D('',#27873,#22646,#22647);
#20491=AXIS2_PLACEMENT_3D('',#27874,#22648,#22649);
#21928=DIRECTION('axis',(0.,0.,1.));
#21929=DIRECTION('refdir',(1.,0.,0.));
#21930=DIRECTION('center_axis',(0.,1.,0.));
#21931=DIRECTION('ref_axis',(1.,0.,0.));
#21932=DIRECTION('',(-1.60844785188215E-15,0.,1.));
#21933=DIRECTION('',(0.707106781186549,0.,0.707106781186546));
#21934=DIRECTION('',(1.,0.,1.55356845212375E-15));
#21935=DIRECTION('',(0.704727298913668,0.,-0.709478283082608));
#21936=DIRECTION('center_axis',(0.,1.,0.));
#21937=DIRECTION('ref_axis',(0.709478283082593,0.,0.704727298913683));
#21938=DIRECTION('',(0.,0.,-1.));
#21939=DIRECTION('center_axis',(0.,1.,0.));
#21940=DIRECTION('ref_axis',(1.,0.,0.));
#21941=DIRECTION('',(-0.702199901316075,0.,-0.711979844231348));
#21942=DIRECTION('center_axis',(0.,-1.,0.));
#21943=DIRECTION('ref_axis',(-0.951733868867053,0.,0.306924490471762));
#21944=DIRECTION('center_axis',(0.,1.,0.));
#21945=DIRECTION('ref_axis',(0.951733868867033,0.,-0.306924490471823));
#21946=DIRECTION('center_axis',(0.,-1.,0.));
#21947=DIRECTION('ref_axis',(-1.,0.,-1.48029736616691E-14));
#21948=DIRECTION('',(1.93287220490857E-14,0.,-1.));
#21949=DIRECTION('center_axis',(0.,-1.,0.));
#21950=DIRECTION('ref_axis',(-0.295138112194515,0.,-0.955454601082782));
#21951=DIRECTION('center_axis',(0.,1.,0.));
#21952=DIRECTION('ref_axis',(0.295138112194494,0.,0.955454601082788));
#21953=DIRECTION('center_axis',(0.,-1.,0.));
#21954=DIRECTION('ref_axis',(-0.710729249896308,0.,-0.703465658964126));
#21955=DIRECTION('',(0.703465658964212,0.,-0.710729249896223));
#21956=DIRECTION('',(1.,0.,6.14369354430926E-16));
#21957=DIRECTION('',(0.703465658964231,0.,0.710729249896204));
#21958=DIRECTION('center_axis',(0.,-1.,0.));
#21959=DIRECTION('ref_axis',(0.963381374692962,0.,-0.26813490428271));
#21960=DIRECTION('center_axis',(0.,1.,0.));
#21961=DIRECTION('ref_axis',(-0.963381374692976,0.,0.268134904282661));
#21962=DIRECTION('center_axis',(0.,-1.,0.));
#21963=DIRECTION('ref_axis',(1.,0.,0.));
#21964=DIRECTION('',(0.,0.,1.));
#21965=DIRECTION('center_axis',(0.,-1.,0.));
#21966=DIRECTION('ref_axis',(0.245760053518526,0.,0.969330694909932));
#21967=DIRECTION('center_axis',(0.,1.,0.));
#21968=DIRECTION('ref_axis',(-0.245760053518557,0.,-0.969330694909924));
#21969=DIRECTION('center_axis',(0.,-1.,0.));
#21970=DIRECTION('ref_axis',(0.711979844231347,0.,0.702199901316076));
#21971=DIRECTION('',(-0.702199901316085,0.,0.711979844231338));
#21972=DIRECTION('center_axis',(0.,1.,0.));
#21973=DIRECTION('ref_axis',(-0.711979844231317,0.,-0.702199901316106));
#21974=DIRECTION('',(1.18143967662125E-14,0.,1.));
#21975=DIRECTION('center_axis',(0.,1.,0.));
#21976=DIRECTION('ref_axis',(-1.,0.,-7.19001577852613E-14));
#21977=DIRECTION('',(0.70472729891367,0.,0.709478283082607));
#21978=DIRECTION('',(1.,0.,0.));
#21979=DIRECTION('',(0.707106781186549,0.,-0.707106781186546));
#21980=DIRECTION('',(0.,0.,-1.));
#21981=DIRECTION('',(-0.707106781186548,0.,-0.707106781186548));
#21982=DIRECTION('',(-1.,0.,0.));
#21983=DIRECTION('',(-0.707106781186551,0.,0.707106781186544));
#21984=DIRECTION('center_axis',(0.710729249896204,0.,-0.703465658964231));
#21985=DIRECTION('ref_axis',(0.703465658964231,0.,0.710729249896204));
#21986=DIRECTION('',(0.,-1.,0.));
#21987=DIRECTION('',(0.703465658964231,0.,0.710729249896204));
#21988=DIRECTION('',(0.,-1.,0.));
#21989=DIRECTION('center_axis',(0.,1.,0.));
#21990=DIRECTION('ref_axis',(0.963381374692962,0.,-0.26813490428271));
#21991=DIRECTION('center_axis',(0.,-1.,0.));
#21992=DIRECTION('ref_axis',(0.963381374692962,0.,-0.26813490428271));
#21993=DIRECTION('',(0.,-1.,0.));
#21994=DIRECTION('center_axis',(0.,1.,0.));
#21995=DIRECTION('ref_axis',(-0.963381374692976,0.,0.268134904282661));
#21996=DIRECTION('center_axis',(0.,1.,0.));
#21997=DIRECTION('ref_axis',(-0.963381374692976,0.,0.268134904282661));
#21998=DIRECTION('',(0.,-1.,0.));
#21999=DIRECTION('center_axis',(0.,1.,0.));
#22000=DIRECTION('ref_axis',(1.,0.,0.));
#22001=DIRECTION('center_axis',(0.,-1.,0.));
#22002=DIRECTION('ref_axis',(1.,0.,0.));
#22003=DIRECTION('',(0.,-1.,0.));
#22004=DIRECTION('center_axis',(1.,0.,0.));
#22005=DIRECTION('ref_axis',(0.,0.,1.));
#22006=DIRECTION('',(0.,0.,1.));
#22007=DIRECTION('',(0.,-1.,0.));
#22008=DIRECTION('center_axis',(0.,1.,0.));
#22009=DIRECTION('ref_axis',(0.245760053518526,0.,0.969330694909932));
#22010=DIRECTION('center_axis',(0.,-1.,0.));
#22011=DIRECTION('ref_axis',(0.245760053518526,0.,0.969330694909932));
#22012=DIRECTION('',(0.,-1.,0.));
#22013=DIRECTION('center_axis',(0.,1.,0.));
#22014=DIRECTION('ref_axis',(-0.245760053518557,0.,-0.969330694909924));
#22015=DIRECTION('center_axis',(0.,1.,0.));
#22016=DIRECTION('ref_axis',(-0.245760053518557,0.,-0.969330694909924));
#22017=DIRECTION('',(0.,-1.,0.));
#22018=DIRECTION('center_axis',(0.,1.,0.));
#22019=DIRECTION('ref_axis',(0.711979844231347,0.,0.702199901316076));
#22020=DIRECTION('center_axis',(0.,-1.,0.));
#22021=DIRECTION('ref_axis',(0.711979844231347,0.,0.702199901316076));
#22022=DIRECTION('',(0.,-1.,0.));
#22023=DIRECTION('center_axis',(0.711979844231338,0.,0.702199901316085));
#22024=DIRECTION('ref_axis',(-0.702199901316085,0.,0.711979844231338));
#22025=DIRECTION('',(-0.702199901316085,0.,0.711979844231338));
#22026=DIRECTION('',(0.,-1.,0.));
#22027=DIRECTION('center_axis',(0.,1.,0.));
#22028=DIRECTION('ref_axis',(-0.711979844231317,0.,-0.702199901316106));
#22029=DIRECTION('center_axis',(0.,1.,0.));
#22030=DIRECTION('ref_axis',(-0.711979844231317,0.,-0.702199901316106));
#22031=DIRECTION('',(0.,-1.,0.));
#22032=DIRECTION('center_axis',(1.,0.,-1.18143967662125E-14));
#22033=DIRECTION('ref_axis',(1.18143967662125E-14,0.,1.));
#22034=DIRECTION('',(1.18143967662125E-14,0.,1.));
#22035=DIRECTION('',(0.,-1.,0.));
#22036=DIRECTION('center_axis',(0.,1.,0.));
#22037=DIRECTION('ref_axis',(-1.,0.,-7.19001577852613E-14));
#22038=DIRECTION('center_axis',(0.,1.,0.));
#22039=DIRECTION('ref_axis',(-1.,0.,-7.19001577852613E-14));
#22040=DIRECTION('',(0.,-1.,0.));
#22041=DIRECTION('center_axis',(0.709478283082607,0.,-0.70472729891367));
#22042=DIRECTION('ref_axis',(0.70472729891367,0.,0.709478283082607));
#22043=DIRECTION('',(0.70472729891367,0.,0.709478283082607));
#22044=DIRECTION('',(0.,-1.,0.));
#22045=DIRECTION('center_axis',(0.,0.,-1.));
#22046=DIRECTION('ref_axis',(1.,0.,0.));
#22047=DIRECTION('',(1.,0.,0.));
#22048=DIRECTION('',(0.,-1.,0.));
#22049=DIRECTION('center_axis',(-0.707106781186546,0.,-0.707106781186549));
#22050=DIRECTION('ref_axis',(0.707106781186549,0.,-0.707106781186546));
#22051=DIRECTION('',(0.707106781186549,0.,-0.707106781186546));
#22052=DIRECTION('',(0.,-1.,0.));
#22053=DIRECTION('center_axis',(-1.,0.,0.));
#22054=DIRECTION('ref_axis',(0.,0.,-1.));
#22055=DIRECTION('',(0.,0.,-1.));
#22056=DIRECTION('',(0.,-1.,0.));
#22057=DIRECTION('center_axis',(1.,0.,1.60844785188215E-15));
#22058=DIRECTION('ref_axis',(-1.60844785188215E-15,0.,1.));
#22059=DIRECTION('',(0.,-1.,0.));
#22060=DIRECTION('',(-1.60844785188215E-15,0.,1.));
#22061=DIRECTION('',(0.,-1.,0.));
#22062=DIRECTION('center_axis',(0.707106781186546,0.,-0.707106781186549));
#22063=DIRECTION('ref_axis',(0.707106781186549,0.,0.707106781186546));
#22064=DIRECTION('',(0.707106781186549,0.,0.707106781186546));
#22065=DIRECTION('',(0.,-1.,0.));
#22066=DIRECTION('center_axis',(1.55356845212375E-15,0.,-1.));
#22067=DIRECTION('ref_axis',(1.,0.,1.55356845212375E-15));
#22068=DIRECTION('',(1.,0.,1.55356845212375E-15));
#22069=DIRECTION('',(0.,-1.,0.));
#22070=DIRECTION('center_axis',(-0.709478283082608,0.,-0.704727298913668));
#22071=DIRECTION('ref_axis',(0.704727298913668,0.,-0.709478283082608));
#22072=DIRECTION('',(0.704727298913668,0.,-0.709478283082608));
#22073=DIRECTION('',(0.,-1.,0.));
#22074=DIRECTION('center_axis',(0.,1.,0.));
#22075=DIRECTION('ref_axis',(0.709478283082593,0.,0.704727298913683));
#22076=DIRECTION('center_axis',(0.,1.,0.));
#22077=DIRECTION('ref_axis',(0.709478283082593,0.,0.704727298913683));
#22078=DIRECTION('',(0.,-1.,0.));
#22079=DIRECTION('center_axis',(-0.707106781186548,0.,0.707106781186548));
#22080=DIRECTION('ref_axis',(-0.707106781186548,0.,-0.707106781186548));
#22081=DIRECTION('',(-0.707106781186548,0.,-0.707106781186548));
#22082=DIRECTION('',(0.,-1.,0.));
#22083=DIRECTION('center_axis',(0.,0.,1.));
#22084=DIRECTION('ref_axis',(-1.,0.,0.));
#22085=DIRECTION('',(-1.,0.,0.));
#22086=DIRECTION('',(0.,-1.,0.));
#22087=DIRECTION('center_axis',(0.707106781186544,0.,0.707106781186551));
#22088=DIRECTION('ref_axis',(-0.707106781186551,0.,0.707106781186544));
#22089=DIRECTION('',(-0.707106781186551,0.,0.707106781186544));
#22090=DIRECTION('center_axis',(-1.,0.,0.));
#22091=DIRECTION('ref_axis',(0.,0.,-1.));
#22092=DIRECTION('',(0.,0.,-1.));
#22093=DIRECTION('',(0.,1.,0.));
#22094=DIRECTION('center_axis',(6.14369354430926E-16,0.,-1.));
#22095=DIRECTION('ref_axis',(1.,0.,6.14369354430926E-16));
#22096=DIRECTION('',(0.,-1.,0.));
#22097=DIRECTION('',(1.,0.,6.14369354430926E-16));
#22098=DIRECTION('center_axis',(-0.710729249896223,0.,-0.703465658964212));
#22099=DIRECTION('ref_axis',(0.703465658964212,0.,-0.710729249896223));
#22100=DIRECTION('',(0.,-1.,0.));
#22101=DIRECTION('',(0.703465658964212,0.,-0.710729249896223));
#22102=DIRECTION('center_axis',(0.,1.,0.));
#22103=DIRECTION('ref_axis',(-0.710729249896308,0.,-0.703465658964126));
#22104=DIRECTION('',(0.,-1.,0.));
#22105=DIRECTION('center_axis',(0.,-1.,0.));
#22106=DIRECTION('ref_axis',(-0.710729249896308,0.,-0.703465658964126));
#22107=DIRECTION('center_axis',(0.,1.,0.));
#22108=DIRECTION('ref_axis',(0.295138112194494,0.,0.955454601082788));
#22109=DIRECTION('',(0.,-1.,0.));
#22110=DIRECTION('center_axis',(0.,1.,0.));
#22111=DIRECTION('ref_axis',(0.295138112194494,0.,0.955454601082788));
#22112=DIRECTION('center_axis',(0.,1.,0.));
#22113=DIRECTION('ref_axis',(-0.295138112194515,0.,-0.955454601082782));
#22114=DIRECTION('',(0.,-1.,0.));
#22115=DIRECTION('center_axis',(0.,-1.,0.));
#22116=DIRECTION('ref_axis',(-0.295138112194515,0.,-0.955454601082782));
#22117=DIRECTION('center_axis',(-1.,0.,-1.93287220490857E-14));
#22118=DIRECTION('ref_axis',(1.93287220490857E-14,0.,-1.));
#22119=DIRECTION('',(0.,-1.,0.));
#22120=DIRECTION('',(1.93287220490857E-14,0.,-1.));
#22121=DIRECTION('center_axis',(0.,1.,0.));
#22122=DIRECTION('ref_axis',(-1.,0.,-1.48029736616691E-14));
#22123=DIRECTION('',(0.,-1.,0.));
#22124=DIRECTION('center_axis',(0.,-1.,0.));
#22125=DIRECTION('ref_axis',(-1.,0.,-1.48029736616691E-14));
#22126=DIRECTION('center_axis',(0.,1.,0.));
#22127=DIRECTION('ref_axis',(0.951733868867033,0.,-0.306924490471823));
#22128=DIRECTION('',(0.,-1.,0.));
#22129=DIRECTION('center_axis',(0.,1.,0.));
#22130=DIRECTION('ref_axis',(0.951733868867033,0.,-0.306924490471823));
#22131=DIRECTION('center_axis',(0.,1.,0.));
#22132=DIRECTION('ref_axis',(-0.951733868867053,0.,0.306924490471762));
#22133=DIRECTION('',(0.,-1.,0.));
#22134=DIRECTION('center_axis',(0.,-1.,0.));
#22135=DIRECTION('ref_axis',(-0.951733868867053,0.,0.306924490471762));
#22136=DIRECTION('center_axis',(-0.711979844231348,0.,0.702199901316075));
#22137=DIRECTION('ref_axis',(-0.702199901316075,0.,-0.711979844231348));
#22138=DIRECTION('',(0.,-1.,0.));
#22139=DIRECTION('',(-0.702199901316075,0.,-0.711979844231348));
#22140=DIRECTION('center_axis',(0.,1.,0.));
#22141=DIRECTION('ref_axis',(1.,0.,0.));
#22142=DIRECTION('center_axis',(0.,1.,0.));
#22143=DIRECTION('ref_axis',(1.,0.,0.));
#22144=DIRECTION('center_axis',(0.,1.,0.));
#22145=DIRECTION('ref_axis',(-1.,0.,0.));
#22146=DIRECTION('center_axis',(0.710729249896204,0.,-0.703465658964231));
#22147=DIRECTION('ref_axis',(0.703465658964231,0.,0.710729249896204));
#22148=DIRECTION('',(0.703465658964231,0.,0.710729249896204));
#22149=DIRECTION('',(0.,-1.,0.));
#22150=DIRECTION('',(0.703465658964231,0.,0.710729249896204));
#22151=DIRECTION('',(0.,-1.,0.));
#22152=DIRECTION('center_axis',(0.,1.,0.));
#22153=DIRECTION('ref_axis',(0.963381374692962,0.,-0.26813490428271));
#22154=DIRECTION('center_axis',(0.,-1.,0.));
#22155=DIRECTION('ref_axis',(0.963381374692962,0.,-0.26813490428271));
#22156=DIRECTION('',(0.,-1.,0.));
#22157=DIRECTION('center_axis',(0.,-1.,0.));
#22158=DIRECTION('ref_axis',(0.963381374692962,0.,-0.26813490428271));
#22159=DIRECTION('center_axis',(0.,1.,0.));
#22160=DIRECTION('ref_axis',(-0.963381374692976,0.,0.268134904282661));
#22161=DIRECTION('center_axis',(0.,1.,0.));
#22162=DIRECTION('ref_axis',(-0.963381374692976,0.,0.268134904282661));
#22163=DIRECTION('',(0.,-1.,0.));
#22164=DIRECTION('center_axis',(0.,1.,0.));
#22165=DIRECTION('ref_axis',(-0.963381374692976,0.,0.268134904282661));
#22166=DIRECTION('center_axis',(0.,1.,0.));
#22167=DIRECTION('ref_axis',(1.,0.,0.));
#22168=DIRECTION('center_axis',(0.,-1.,0.));
#22169=DIRECTION('ref_axis',(1.,0.,0.));
#22170=DIRECTION('',(0.,-1.,0.));
#22171=DIRECTION('center_axis',(0.,-1.,0.));
#22172=DIRECTION('ref_axis',(1.,0.,0.));
#22173=DIRECTION('center_axis',(1.,0.,0.));
#22174=DIRECTION('ref_axis',(0.,0.,1.));
#22175=DIRECTION('',(0.,0.,1.));
#22176=DIRECTION('',(0.,-1.,0.));
#22177=DIRECTION('',(0.,0.,1.));
#22178=DIRECTION('center_axis',(0.,1.,0.));
#22179=DIRECTION('ref_axis',(0.245760053518526,0.,0.969330694909932));
#22180=DIRECTION('center_axis',(0.,-1.,0.));
#22181=DIRECTION('ref_axis',(0.245760053518526,0.,0.969330694909932));
#22182=DIRECTION('',(0.,-1.,0.));
#22183=DIRECTION('center_axis',(0.,-1.,0.));
#22184=DIRECTION('ref_axis',(0.245760053518526,0.,0.969330694909932));
#22185=DIRECTION('center_axis',(0.,1.,0.));
#22186=DIRECTION('ref_axis',(-0.245760053518557,0.,-0.969330694909924));
#22187=DIRECTION('center_axis',(0.,1.,0.));
#22188=DIRECTION('ref_axis',(-0.245760053518557,0.,-0.969330694909924));
#22189=DIRECTION('',(0.,-1.,0.));
#22190=DIRECTION('center_axis',(0.,1.,0.));
#22191=DIRECTION('ref_axis',(-0.245760053518557,0.,-0.969330694909924));
#22192=DIRECTION('center_axis',(0.,1.,0.));
#22193=DIRECTION('ref_axis',(-1.,0.,0.));
#22194=DIRECTION('',(0.707106781186554,0.,-0.707106781186541));
#22195=DIRECTION('',(0.,0.,-1.));
#22196=DIRECTION('',(0.707106781186549,0.,-0.707106781186546));
#22197=DIRECTION('',(1.,0.,0.));
#22198=DIRECTION('',(0.70472729891367,0.,0.709478283082607));
#22199=DIRECTION('center_axis',(0.,1.,0.));
#22200=DIRECTION('ref_axis',(-1.,0.,-7.19001577852613E-14));
#22201=DIRECTION('',(1.18143967662125E-14,0.,1.));
#22202=DIRECTION('center_axis',(0.,1.,0.));
#22203=DIRECTION('ref_axis',(-0.711979844231317,0.,-0.702199901316106));
#22204=DIRECTION('',(-0.702199901316085,0.,0.711979844231338));
#22205=DIRECTION('center_axis',(0.,-1.,0.));
#22206=DIRECTION('ref_axis',(0.711979844231347,0.,0.702199901316076));
#22207=DIRECTION('',(1.,0.,6.14369354430926E-16));
#22208=DIRECTION('',(0.703465658964212,0.,-0.710729249896223));
#22209=DIRECTION('center_axis',(0.,-1.,0.));
#22210=DIRECTION('ref_axis',(-0.710729249896308,0.,-0.703465658964126));
#22211=DIRECTION('center_axis',(0.,1.,0.));
#22212=DIRECTION('ref_axis',(0.295138112194494,0.,0.955454601082788));
#22213=DIRECTION('center_axis',(0.,-1.,0.));
#22214=DIRECTION('ref_axis',(-0.295138112194515,0.,-0.955454601082782));
#22215=DIRECTION('',(1.93287220490857E-14,0.,-1.));
#22216=DIRECTION('center_axis',(0.,-1.,0.));
#22217=DIRECTION('ref_axis',(-1.,0.,-1.48029736616691E-14));
#22218=DIRECTION('center_axis',(0.,1.,0.));
#22219=DIRECTION('ref_axis',(0.951733868867033,0.,-0.306924490471823));
#22220=DIRECTION('center_axis',(0.,-1.,0.));
#22221=DIRECTION('ref_axis',(-0.951733868867053,0.,0.306924490471762));
#22222=DIRECTION('',(-0.702199901316075,0.,-0.711979844231348));
#22223=DIRECTION('center_axis',(0.,1.,0.));
#22224=DIRECTION('ref_axis',(1.,0.,0.));
#22225=DIRECTION('',(0.,0.,-1.));
#22226=DIRECTION('center_axis',(0.,1.,0.));
#22227=DIRECTION('ref_axis',(0.709478283082593,0.,0.704727298913683));
#22228=DIRECTION('',(0.704727298913668,0.,-0.709478283082608));
#22229=DIRECTION('',(1.,0.,1.55356845212375E-15));
#22230=DIRECTION('',(0.707106781186549,0.,0.707106781186546));
#22231=DIRECTION('',(-1.60844785188215E-15,0.,1.));
#22232=DIRECTION('',(-0.707106781186556,0.,-0.707106781186539));
#22233=DIRECTION('',(-2.63040290597841E-15,0.,-1.));
#22234=DIRECTION('',(0.707106781186546,0.,-0.707106781186549));
#22235=DIRECTION('',(1.,0.,-2.63040290597841E-15));
#22236=DIRECTION('center_axis',(0.,1.,0.));
#22237=DIRECTION('ref_axis',(-1.37675000001205E-14,0.,1.));
#22238=DIRECTION('',(-1.,0.,0.));
#22239=DIRECTION('center_axis',(0.,-1.,0.));
#22240=DIRECTION('ref_axis',(1.63979029060989E-14,0.,1.));
#22241=DIRECTION('',(-1.,0.,0.));
#22242=DIRECTION('',(-0.707106781186548,0.,-0.707106781186548));
#22243=DIRECTION('',(0.,0.,-1.));
#22244=DIRECTION('center_axis',(-0.707106781186541,0.,-0.707106781186554));
#22245=DIRECTION('ref_axis',(0.707106781186554,0.,-0.707106781186541));
#22246=DIRECTION('',(0.,-1.,0.));
#22247=DIRECTION('',(-0.707106781186554,0.,0.707106781186541));
#22248=DIRECTION('',(0.,-1.,0.));
#22249=DIRECTION('center_axis',(-1.,0.,0.));
#22250=DIRECTION('ref_axis',(0.,0.,-1.));
#22251=DIRECTION('',(0.,-1.,0.));
#22252=DIRECTION('',(0.,0.,1.));
#22253=DIRECTION('center_axis',(-0.707106781186548,0.,0.707106781186548));
#22254=DIRECTION('ref_axis',(-0.707106781186548,0.,-0.707106781186548));
#22255=DIRECTION('',(0.,-1.,0.));
#22256=DIRECTION('',(0.707106781186548,0.,0.707106781186548));
#22257=DIRECTION('center_axis',(0.,0.,1.));
#22258=DIRECTION('ref_axis',(-1.,0.,0.));
#22259=DIRECTION('',(0.,-1.,0.));
#22260=DIRECTION('',(1.,0.,0.));
#22261=DIRECTION('center_axis',(0.,0.,-1.));
#22262=DIRECTION('ref_axis',(-1.,0.,0.));
#22263=DIRECTION('center_axis',(0.,0.,-1.));
#22264=DIRECTION('ref_axis',(-1.,0.,0.));
#22265=DIRECTION('center_axis',(0.,1.,0.));
#22266=DIRECTION('ref_axis',(1.63979029060989E-14,0.,1.));
#22267=DIRECTION('',(0.,-1.,0.));
#22268=DIRECTION('center_axis',(0.,1.,0.));
#22269=DIRECTION('ref_axis',(1.63979029060989E-14,0.,1.));
#22270=DIRECTION('center_axis',(0.,0.,1.));
#22271=DIRECTION('ref_axis',(-1.,0.,0.));
#22272=DIRECTION('',(0.,-1.,0.));
#22273=DIRECTION('',(-1.,0.,2.63040290597841E-15));
#22274=DIRECTION('center_axis',(0.,1.,0.));
#22275=DIRECTION('ref_axis',(-1.,0.,0.));
#22276=DIRECTION('center_axis',(0.,-1.,0.));
#22277=DIRECTION('ref_axis',(-1.37675000001205E-14,0.,1.));
#22278=DIRECTION('',(-1.,0.,2.63040290597841E-15));
#22279=DIRECTION('',(-0.707106781186546,0.,0.707106781186549));
#22280=DIRECTION('',(2.63040290597841E-15,0.,1.));
#22281=DIRECTION('',(0.707106781186556,0.,0.707106781186539));
#22282=DIRECTION('',(-1.60844785188215E-15,0.,1.));
#22283=DIRECTION('',(0.707106781186549,0.,0.707106781186546));
#22284=DIRECTION('',(1.,0.,1.55356845212375E-15));
#22285=DIRECTION('',(0.704727298913668,0.,-0.709478283082608));
#22286=DIRECTION('center_axis',(0.,1.,0.));
#22287=DIRECTION('ref_axis',(0.709478283082593,0.,0.704727298913683));
#22288=DIRECTION('',(0.,0.,-1.));
#22289=DIRECTION('center_axis',(0.,1.,0.));
#22290=DIRECTION('ref_axis',(1.,0.,0.));
#22291=DIRECTION('',(-0.702199901316075,0.,-0.711979844231348));
#22292=DIRECTION('center_axis',(0.,-1.,0.));
#22293=DIRECTION('ref_axis',(-0.951733868867053,0.,0.306924490471762));
#22294=DIRECTION('center_axis',(0.,1.,0.));
#22295=DIRECTION('ref_axis',(0.951733868867033,0.,-0.306924490471823));
#22296=DIRECTION('center_axis',(0.,-1.,0.));
#22297=DIRECTION('ref_axis',(-1.,0.,-1.48029736616691E-14));
#22298=DIRECTION('',(1.93287220490857E-14,0.,-1.));
#22299=DIRECTION('center_axis',(0.,-1.,0.));
#22300=DIRECTION('ref_axis',(-0.295138112194515,0.,-0.955454601082782));
#22301=DIRECTION('center_axis',(0.,1.,0.));
#22302=DIRECTION('ref_axis',(0.295138112194494,0.,0.955454601082788));
#22303=DIRECTION('center_axis',(0.,-1.,0.));
#22304=DIRECTION('ref_axis',(-0.710729249896308,0.,-0.703465658964126));
#22305=DIRECTION('',(0.703465658964212,0.,-0.710729249896223));
#22306=DIRECTION('',(1.,0.,6.14369354430926E-16));
#22307=DIRECTION('center_axis',(0.,-1.,0.));
#22308=DIRECTION('ref_axis',(0.711979844231347,0.,0.702199901316076));
#22309=DIRECTION('',(-0.702199901316085,0.,0.711979844231338));
#22310=DIRECTION('center_axis',(0.,1.,0.));
#22311=DIRECTION('ref_axis',(-0.711979844231317,0.,-0.702199901316106));
#22312=DIRECTION('',(1.18143967662125E-14,0.,1.));
#22313=DIRECTION('center_axis',(0.,1.,0.));
#22314=DIRECTION('ref_axis',(-1.,0.,-7.19001577852613E-14));
#22315=DIRECTION('',(0.70472729891367,0.,0.709478283082607));
#22316=DIRECTION('',(1.,0.,0.));
#22317=DIRECTION('',(0.707106781186549,0.,-0.707106781186546));
#22318=DIRECTION('',(0.,0.,-1.));
#22319=DIRECTION('center_axis',(-0.707106781186539,0.,0.707106781186556));
#22320=DIRECTION('ref_axis',(-0.707106781186556,0.,-0.707106781186539));
#22321=DIRECTION('',(0.,-1.,0.));
#22322=DIRECTION('',(0.,1.,0.));
#22323=DIRECTION('center_axis',(-1.,0.,2.63040290597841E-15));
#22324=DIRECTION('ref_axis',(-2.63040290597841E-15,0.,-1.));
#22325=DIRECTION('',(0.,-1.,0.));
#22326=DIRECTION('center_axis',(-0.707106781186549,0.,-0.707106781186546));
#22327=DIRECTION('ref_axis',(0.707106781186546,0.,-0.707106781186549));
#22328=DIRECTION('',(0.,-1.,0.));
#22329=DIRECTION('center_axis',(-2.63040290597841E-15,0.,-1.));
#22330=DIRECTION('ref_axis',(1.,0.,-2.63040290597841E-15));
#22331=DIRECTION('',(0.,-1.,0.));
#22332=DIRECTION('center_axis',(-2.63040290597841E-15,0.,-1.));
#22333=DIRECTION('ref_axis',(-1.,0.,0.));
#22334=DIRECTION('center_axis',(-2.63040290597841E-15,0.,-1.));
#22335=DIRECTION('ref_axis',(-1.,0.,0.));
#22336=DIRECTION('center_axis',(0.,-1.,0.));
#22337=DIRECTION('ref_axis',(-1.37675000001205E-14,0.,1.));
#22338=DIRECTION('center_axis',(0.,0.,-1.));
#22339=DIRECTION('ref_axis',(-1.,0.,0.));
#22340=DIRECTION('',(0.,0.,1.));
#22341=DIRECTION('center_axis',(0.,0.,1.));
#22342=DIRECTION('ref_axis',(-1.,0.,0.));
#22343=DIRECTION('center_axis',(0.,0.,-1.));
#22344=DIRECTION('ref_axis',(-1.,0.,0.));
#22345=DIRECTION('',(0.,0.,1.));
#22346=DIRECTION('center_axis',(-1.55356845212375E-15,0.,1.));
#22347=DIRECTION('ref_axis',(-1.,0.,0.));
#22348=DIRECTION('center_axis',(0.,0.,-1.));
#22349=DIRECTION('ref_axis',(-1.,0.,0.));
#22350=DIRECTION('',(0.,0.,1.));
#22351=DIRECTION('center_axis',(0.,0.,1.));
#22352=DIRECTION('ref_axis',(-1.,0.,0.));
#22353=DIRECTION('center_axis',(0.,0.,-1.));
#22354=DIRECTION('ref_axis',(-1.,0.,0.));
#22355=DIRECTION('',(0.,0.,1.));
#22356=DIRECTION('center_axis',(-1.55356845212375E-15,0.,1.));
#22357=DIRECTION('ref_axis',(-1.,0.,0.));
#22358=DIRECTION('center_axis',(-1.,0.,0.));
#22359=DIRECTION('ref_axis',(0.,0.,-1.));
#22360=DIRECTION('',(0.,-1.,0.));
#22361=DIRECTION('center_axis',(-0.707106781186546,0.,-0.707106781186549));
#22362=DIRECTION('ref_axis',(0.707106781186549,0.,-0.707106781186546));
#22363=DIRECTION('',(0.,-1.,0.));
#22364=DIRECTION('center_axis',(0.,0.,-1.));
#22365=DIRECTION('ref_axis',(1.,0.,0.));
#22366=DIRECTION('',(0.,-1.,0.));
#22367=DIRECTION('center_axis',(0.709478283082607,0.,-0.70472729891367));
#22368=DIRECTION('ref_axis',(0.70472729891367,0.,0.709478283082607));
#22369=DIRECTION('',(0.,-1.,0.));
#22370=DIRECTION('center_axis',(0.,1.,0.));
#22371=DIRECTION('ref_axis',(-1.,0.,-7.19001577852613E-14));
#22372=DIRECTION('',(0.,-1.,0.));
#22373=DIRECTION('center_axis',(1.,0.,-1.18143967662125E-14));
#22374=DIRECTION('ref_axis',(1.18143967662125E-14,0.,1.));
#22375=DIRECTION('',(0.,-1.,0.));
#22376=DIRECTION('center_axis',(0.,1.,0.));
#22377=DIRECTION('ref_axis',(-0.711979844231317,0.,-0.702199901316106));
#22378=DIRECTION('',(0.,-1.,0.));
#22379=DIRECTION('center_axis',(0.711979844231338,0.,0.702199901316085));
#22380=DIRECTION('ref_axis',(-0.702199901316085,0.,0.711979844231338));
#22381=DIRECTION('',(0.,-1.,0.));
#22382=DIRECTION('center_axis',(0.,1.,0.));
#22383=DIRECTION('ref_axis',(0.711979844231347,0.,0.702199901316076));
#22384=DIRECTION('center_axis',(1.,0.,1.60844785188215E-15));
#22385=DIRECTION('ref_axis',(-1.60844785188215E-15,0.,1.));
#22386=DIRECTION('',(0.,-1.,0.));
#22387=DIRECTION('center_axis',(0.707106781186546,0.,-0.707106781186549));
#22388=DIRECTION('ref_axis',(0.707106781186549,0.,0.707106781186546));
#22389=DIRECTION('',(0.,-1.,0.));
#22390=DIRECTION('center_axis',(1.55356845212375E-15,0.,-1.));
#22391=DIRECTION('ref_axis',(1.,0.,1.55356845212375E-15));
#22392=DIRECTION('',(0.,-1.,0.));
#22393=DIRECTION('center_axis',(-0.709478283082608,0.,-0.704727298913668));
#22394=DIRECTION('ref_axis',(0.704727298913668,0.,-0.709478283082608));
#22395=DIRECTION('',(0.,-1.,0.));
#22396=DIRECTION('center_axis',(0.,1.,0.));
#22397=DIRECTION('ref_axis',(0.709478283082593,0.,0.704727298913683));
#22398=DIRECTION('',(0.,-1.,0.));
#22399=DIRECTION('center_axis',(-1.,0.,0.));
#22400=DIRECTION('ref_axis',(0.,0.,-1.));
#22401=DIRECTION('',(0.,1.,0.));
#22402=DIRECTION('center_axis',(0.,1.,0.));
#22403=DIRECTION('ref_axis',(1.,0.,0.));
#22404=DIRECTION('',(0.,-1.,0.));
#22405=DIRECTION('center_axis',(-0.711979844231348,0.,0.702199901316075));
#22406=DIRECTION('ref_axis',(-0.702199901316075,0.,-0.711979844231348));
#22407=DIRECTION('',(0.,-1.,0.));
#22408=DIRECTION('center_axis',(0.,1.,0.));
#22409=DIRECTION('ref_axis',(-0.951733868867053,0.,0.306924490471762));
#22410=DIRECTION('',(0.,-1.,0.));
#22411=DIRECTION('center_axis',(0.,1.,0.));
#22412=DIRECTION('ref_axis',(0.951733868867033,0.,-0.306924490471823));
#22413=DIRECTION('',(0.,-1.,0.));
#22414=DIRECTION('center_axis',(0.,1.,0.));
#22415=DIRECTION('ref_axis',(-1.,0.,-1.48029736616691E-14));
#22416=DIRECTION('',(0.,-1.,0.));
#22417=DIRECTION('center_axis',(-1.,0.,-1.93287220490857E-14));
#22418=DIRECTION('ref_axis',(1.93287220490857E-14,0.,-1.));
#22419=DIRECTION('',(0.,-1.,0.));
#22420=DIRECTION('center_axis',(0.,1.,0.));
#22421=DIRECTION('ref_axis',(-0.295138112194515,0.,-0.955454601082782));
#22422=DIRECTION('',(0.,-1.,0.));
#22423=DIRECTION('center_axis',(0.,1.,0.));
#22424=DIRECTION('ref_axis',(0.295138112194494,0.,0.955454601082788));
#22425=DIRECTION('',(0.,-1.,0.));
#22426=DIRECTION('center_axis',(0.,1.,0.));
#22427=DIRECTION('ref_axis',(-0.710729249896308,0.,-0.703465658964126));
#22428=DIRECTION('',(0.,-1.,0.));
#22429=DIRECTION('center_axis',(-0.710729249896223,0.,-0.703465658964212));
#22430=DIRECTION('ref_axis',(0.703465658964212,0.,-0.710729249896223));
#22431=DIRECTION('',(0.,-1.,0.));
#22432=DIRECTION('center_axis',(6.14369354430926E-16,0.,-1.));
#22433=DIRECTION('ref_axis',(1.,0.,6.14369354430926E-16));
#22434=DIRECTION('center_axis',(0.,1.,0.));
#22435=DIRECTION('ref_axis',(0.711979844231347,0.,0.702199901316076));
#22436=DIRECTION('center_axis',(0.,-1.,0.));
#22437=DIRECTION('ref_axis',(0.711979844231347,0.,0.702199901316076));
#22438=DIRECTION('',(0.,-1.,0.));
#22439=DIRECTION('center_axis',(0.,1.,0.));
#22440=DIRECTION('ref_axis',(0.711979844231347,0.,0.702199901316076));
#22441=DIRECTION('',(0.,-1.,0.));
#22442=DIRECTION('center_axis',(0.711979844231338,0.,0.702199901316085));
#22443=DIRECTION('ref_axis',(-0.702199901316085,0.,0.711979844231338));
#22444=DIRECTION('',(-0.702199901316085,0.,0.711979844231338));
#22445=DIRECTION('',(0.,-1.,0.));
#22446=DIRECTION('',(0.702199901316085,0.,-0.711979844231338));
#22447=DIRECTION('center_axis',(0.,1.,0.));
#22448=DIRECTION('ref_axis',(-0.711979844231317,0.,-0.702199901316106));
#22449=DIRECTION('center_axis',(0.,1.,0.));
#22450=DIRECTION('ref_axis',(-0.711979844231317,0.,-0.702199901316106));
#22451=DIRECTION('',(0.,-1.,0.));
#22452=DIRECTION('center_axis',(0.,-1.,0.));
#22453=DIRECTION('ref_axis',(-0.711979844231317,0.,-0.702199901316106));
#22454=DIRECTION('center_axis',(1.,0.,-1.18143967662125E-14));
#22455=DIRECTION('ref_axis',(1.18143967662125E-14,0.,1.));
#22456=DIRECTION('',(1.18143967662125E-14,0.,1.));
#22457=DIRECTION('',(0.,-1.,0.));
#22458=DIRECTION('',(-1.18143967662125E-14,0.,-1.));
#22459=DIRECTION('center_axis',(0.,1.,0.));
#22460=DIRECTION('ref_axis',(-1.,0.,-7.19001577852613E-14));
#22461=DIRECTION('center_axis',(0.,1.,0.));
#22462=DIRECTION('ref_axis',(-1.,0.,-7.19001577852613E-14));
#22463=DIRECTION('',(0.,-1.,0.));
#22464=DIRECTION('center_axis',(0.,-1.,0.));
#22465=DIRECTION('ref_axis',(-1.,0.,-7.19001577852613E-14));
#22466=DIRECTION('center_axis',(0.709478283082607,0.,-0.70472729891367));
#22467=DIRECTION('ref_axis',(0.70472729891367,0.,0.709478283082607));
#22468=DIRECTION('',(0.70472729891367,0.,0.709478283082607));
#22469=DIRECTION('',(0.,-1.,0.));
#22470=DIRECTION('',(-0.70472729891367,0.,-0.709478283082607));
#22471=DIRECTION('center_axis',(0.,0.,-1.));
#22472=DIRECTION('ref_axis',(1.,0.,0.));
#22473=DIRECTION('',(1.,0.,0.));
#22474=DIRECTION('',(0.,-1.,0.));
#22475=DIRECTION('',(-1.,0.,0.));
#22476=DIRECTION('center_axis',(-0.707106781186546,0.,-0.707106781186549));
#22477=DIRECTION('ref_axis',(0.707106781186549,0.,-0.707106781186546));
#22478=DIRECTION('',(0.707106781186549,0.,-0.707106781186546));
#22479=DIRECTION('',(0.,-1.,0.));
#22480=DIRECTION('',(-0.707106781186549,0.,0.707106781186546));
#22481=DIRECTION('center_axis',(-0.707106781186548,0.,0.707106781186548));
#22482=DIRECTION('ref_axis',(-0.707106781186548,0.,-0.707106781186548));
#22483=DIRECTION('',(0.707106781186548,0.,0.707106781186548));
#22484=DIRECTION('',(0.,-1.,0.));
#22485=DIRECTION('',(0.707106781186548,0.,0.707106781186548));
#22486=DIRECTION('',(0.,-1.,0.));
#22487=DIRECTION('center_axis',(0.,0.,1.));
#22488=DIRECTION('ref_axis',(-1.,0.,0.));
#22489=DIRECTION('',(1.,0.,0.));
#22490=DIRECTION('',(0.,-1.,0.));
#22491=DIRECTION('',(1.,0.,0.));
#22492=DIRECTION('center_axis',(0.707106781186544,0.,0.707106781186551));
#22493=DIRECTION('ref_axis',(-0.707106781186551,0.,0.707106781186544));
#22494=DIRECTION('',(0.707106781186551,0.,-0.707106781186544));
#22495=DIRECTION('',(0.,-1.,0.));
#22496=DIRECTION('',(0.707106781186551,0.,-0.707106781186544));
#22497=DIRECTION('center_axis',(1.,0.,1.60844785188215E-15));
#22498=DIRECTION('ref_axis',(-1.60844785188215E-15,0.,1.));
#22499=DIRECTION('',(-1.60844785188215E-15,0.,1.));
#22500=DIRECTION('',(0.,-1.,0.));
#22501=DIRECTION('',(1.60844785188215E-15,0.,-1.));
#22502=DIRECTION('center_axis',(0.707106781186546,0.,-0.707106781186549));
#22503=DIRECTION('ref_axis',(0.707106781186549,0.,0.707106781186546));
#22504=DIRECTION('',(0.707106781186549,0.,0.707106781186546));
#22505=DIRECTION('',(0.,-1.,0.));
#22506=DIRECTION('',(-0.707106781186549,0.,-0.707106781186546));
#22507=DIRECTION('center_axis',(1.55356845212375E-15,0.,-1.));
#22508=DIRECTION('ref_axis',(1.,0.,1.55356845212375E-15));
#22509=DIRECTION('',(1.,0.,1.55356845212375E-15));
#22510=DIRECTION('',(0.,-1.,0.));
#22511=DIRECTION('',(-1.,0.,-1.55356845212375E-15));
#22512=DIRECTION('center_axis',(-0.709478283082608,0.,-0.704727298913668));
#22513=DIRECTION('ref_axis',(0.704727298913668,0.,-0.709478283082608));
#22514=DIRECTION('',(0.704727298913668,0.,-0.709478283082608));
#22515=DIRECTION('',(0.,-1.,0.));
#22516=DIRECTION('',(-0.704727298913668,0.,0.709478283082608));
#22517=DIRECTION('center_axis',(0.,1.,0.));
#22518=DIRECTION('ref_axis',(0.709478283082593,0.,0.704727298913683));
#22519=DIRECTION('center_axis',(0.,1.,0.));
#22520=DIRECTION('ref_axis',(0.709478283082593,0.,0.704727298913683));
#22521=DIRECTION('',(0.,-1.,0.));
#22522=DIRECTION('center_axis',(0.,-1.,0.));
#22523=DIRECTION('ref_axis',(0.709478283082593,0.,0.704727298913683));
#22524=DIRECTION('center_axis',(0.,1.,0.));
#22525=DIRECTION('ref_axis',(-1.,0.,0.));
#22526=DIRECTION('center_axis',(0.,-1.,0.));
#22527=DIRECTION('ref_axis',(1.,0.,0.));
#22528=DIRECTION('',(0.702199901316075,0.,0.711979844231348));
#22529=DIRECTION('center_axis',(0.,1.,0.));
#22530=DIRECTION('ref_axis',(-0.951733868867053,0.,0.306924490471762));
#22531=DIRECTION('center_axis',(0.,-1.,0.));
#22532=DIRECTION('ref_axis',(0.951733868867033,0.,-0.306924490471823));
#22533=DIRECTION('center_axis',(0.,1.,0.));
#22534=DIRECTION('ref_axis',(-1.,0.,-1.48029736616691E-14));
#22535=DIRECTION('',(-1.93287220490857E-14,0.,1.));
#22536=DIRECTION('center_axis',(0.,1.,0.));
#22537=DIRECTION('ref_axis',(-0.295138112194515,0.,-0.955454601082782));
#22538=DIRECTION('center_axis',(0.,-1.,0.));
#22539=DIRECTION('ref_axis',(0.295138112194494,0.,0.955454601082788));
#22540=DIRECTION('center_axis',(0.,1.,0.));
#22541=DIRECTION('ref_axis',(-0.710729249896308,0.,-0.703465658964126));
#22542=DIRECTION('',(-0.703465658964212,0.,0.710729249896223));
#22543=DIRECTION('',(-1.,0.,-6.14369354430926E-16));
#22544=DIRECTION('',(-0.703465658964231,0.,-0.710729249896204));
#22545=DIRECTION('center_axis',(0.,1.,0.));
#22546=DIRECTION('ref_axis',(0.963381374692962,0.,-0.26813490428271));
#22547=DIRECTION('center_axis',(0.,-1.,0.));
#22548=DIRECTION('ref_axis',(-0.963381374692976,0.,0.268134904282661));
#22549=DIRECTION('center_axis',(0.,1.,0.));
#22550=DIRECTION('ref_axis',(1.,0.,0.));
#22551=DIRECTION('',(0.,0.,-1.));
#22552=DIRECTION('center_axis',(0.,1.,0.));
#22553=DIRECTION('ref_axis',(0.245760053518526,0.,0.969330694909932));
#22554=DIRECTION('center_axis',(0.,-1.,0.));
#22555=DIRECTION('ref_axis',(-0.245760053518557,0.,-0.969330694909924));
#22556=DIRECTION('',(0.,0.,1.));
#22557=DIRECTION('',(0.,0.,1.));
#22558=DIRECTION('center_axis',(-1.,0.,0.));
#22559=DIRECTION('ref_axis',(0.,0.,-1.));
#22560=DIRECTION('',(0.,0.,-1.));
#22561=DIRECTION('center_axis',(-1.,0.,0.));
#22562=DIRECTION('ref_axis',(0.,0.,-1.));
#22563=DIRECTION('',(0.,0.,-1.));
#22564=DIRECTION('',(0.,1.,0.));
#22565=DIRECTION('center_axis',(0.,1.,0.));
#22566=DIRECTION('ref_axis',(1.,0.,0.));
#22567=DIRECTION('center_axis',(0.,1.,0.));
#22568=DIRECTION('ref_axis',(1.,0.,0.));
#22569=DIRECTION('',(0.,-1.,0.));
#22570=DIRECTION('center_axis',(-0.711979844231348,0.,0.702199901316075));
#22571=DIRECTION('ref_axis',(-0.702199901316075,0.,-0.711979844231348));
#22572=DIRECTION('',(-0.702199901316075,0.,-0.711979844231348));
#22573=DIRECTION('',(0.,-1.,0.));
#22574=DIRECTION('center_axis',(0.,1.,0.));
#22575=DIRECTION('ref_axis',(-0.951733868867053,0.,0.306924490471762));
#22576=DIRECTION('center_axis',(0.,-1.,0.));
#22577=DIRECTION('ref_axis',(-0.951733868867053,0.,0.306924490471762));
#22578=DIRECTION('',(0.,-1.,0.));
#22579=DIRECTION('center_axis',(0.,1.,0.));
#22580=DIRECTION('ref_axis',(0.951733868867033,0.,-0.306924490471823));
#22581=DIRECTION('center_axis',(0.,1.,0.));
#22582=DIRECTION('ref_axis',(0.951733868867033,0.,-0.306924490471823));
#22583=DIRECTION('',(0.,-1.,0.));
#22584=DIRECTION('center_axis',(0.,1.,0.));
#22585=DIRECTION('ref_axis',(-1.,0.,-1.48029736616691E-14));
#22586=DIRECTION('center_axis',(0.,-1.,0.));
#22587=DIRECTION('ref_axis',(-1.,0.,-1.48029736616691E-14));
#22588=DIRECTION('',(0.,-1.,0.));
#22589=DIRECTION('center_axis',(-1.,0.,-1.93287220490857E-14));
#22590=DIRECTION('ref_axis',(1.93287220490857E-14,0.,-1.));
#22591=DIRECTION('',(1.93287220490857E-14,0.,-1.));
#22592=DIRECTION('',(0.,-1.,0.));
#22593=DIRECTION('center_axis',(0.,1.,0.));
#22594=DIRECTION('ref_axis',(-0.295138112194515,0.,-0.955454601082782));
#22595=DIRECTION('center_axis',(0.,-1.,0.));
#22596=DIRECTION('ref_axis',(-0.295138112194515,0.,-0.955454601082782));
#22597=DIRECTION('',(0.,-1.,0.));
#22598=DIRECTION('center_axis',(0.,1.,0.));
#22599=DIRECTION('ref_axis',(0.295138112194494,0.,0.955454601082788));
#22600=DIRECTION('center_axis',(0.,1.,0.));
#22601=DIRECTION('ref_axis',(0.295138112194494,0.,0.955454601082788));
#22602=DIRECTION('',(0.,-1.,0.));
#22603=DIRECTION('center_axis',(0.,1.,0.));
#22604=DIRECTION('ref_axis',(-0.710729249896308,0.,-0.703465658964126));
#22605=DIRECTION('center_axis',(0.,-1.,0.));
#22606=DIRECTION('ref_axis',(-0.710729249896308,0.,-0.703465658964126));
#22607=DIRECTION('',(0.,-1.,0.));
#22608=DIRECTION('center_axis',(-0.710729249896223,0.,-0.703465658964212));
#22609=DIRECTION('ref_axis',(0.703465658964212,0.,-0.710729249896223));
#22610=DIRECTION('',(0.703465658964212,0.,-0.710729249896223));
#22611=DIRECTION('',(0.,-1.,0.));
#22612=DIRECTION('center_axis',(6.14369354430926E-16,0.,-1.));
#22613=DIRECTION('ref_axis',(1.,0.,6.14369354430926E-16));
#22614=DIRECTION('',(1.,0.,6.14369354430926E-16));
#22615=DIRECTION('',(0.,-1.,0.));
#22616=DIRECTION('center_axis',(0.710729249896204,0.,-0.703465658964231));
#22617=DIRECTION('ref_axis',(0.703465658964231,0.,0.710729249896204));
#22618=DIRECTION('',(0.703465658964231,0.,0.710729249896204));
#22619=DIRECTION('',(0.,-1.,0.));
#22620=DIRECTION('center_axis',(0.,1.,0.));
#22621=DIRECTION('ref_axis',(0.963381374692962,0.,-0.26813490428271));
#22622=DIRECTION('center_axis',(0.,-1.,0.));
#22623=DIRECTION('ref_axis',(0.963381374692962,0.,-0.26813490428271));
#22624=DIRECTION('',(0.,-1.,0.));
#22625=DIRECTION('center_axis',(0.,1.,0.));
#22626=DIRECTION('ref_axis',(-0.963381374692976,0.,0.268134904282661));
#22627=DIRECTION('center_axis',(0.,1.,0.));
#22628=DIRECTION('ref_axis',(-0.963381374692976,0.,0.268134904282661));
#22629=DIRECTION('',(0.,-1.,0.));
#22630=DIRECTION('center_axis',(0.,1.,0.));
#22631=DIRECTION('ref_axis',(1.,0.,0.));
#22632=DIRECTION('center_axis',(0.,-1.,0.));
#22633=DIRECTION('ref_axis',(1.,0.,0.));
#22634=DIRECTION('',(0.,-1.,0.));
#22635=DIRECTION('center_axis',(1.,0.,0.));
#22636=DIRECTION('ref_axis',(0.,0.,1.));
#22637=DIRECTION('',(0.,0.,1.));
#22638=DIRECTION('',(0.,-1.,0.));
#22639=DIRECTION('center_axis',(0.,1.,0.));
#22640=DIRECTION('ref_axis',(0.245760053518526,0.,0.969330694909932));
#22641=DIRECTION('center_axis',(0.,-1.,0.));
#22642=DIRECTION('ref_axis',(0.245760053518526,0.,0.969330694909932));
#22643=DIRECTION('',(0.,-1.,0.));
#22644=DIRECTION('center_axis',(0.,1.,0.));
#22645=DIRECTION('ref_axis',(-0.245760053518557,0.,-0.969330694909924));
#22646=DIRECTION('center_axis',(0.,1.,0.));
#22647=DIRECTION('ref_axis',(-0.245760053518557,0.,-0.969330694909924));
#22648=DIRECTION('center_axis',(0.,1.,0.));
#22649=DIRECTION('ref_axis',(1.,0.,0.));
#27148=CARTESIAN_POINT('',(0.,0.,0.));
#27149=CARTESIAN_POINT('Origin',(103.778785519041,230.,0.));
#27150=CARTESIAN_POINT('',(113.356459668193,230.,-58.0910625167936));
#27151=CARTESIAN_POINT('',(113.356459668193,230.,-36.0032237681315));
#27152=CARTESIAN_POINT('',(113.356459668193,230.,-29.0455312583968));
#27153=CARTESIAN_POINT('',(114.856459668193,230.,-34.5032237681315));
#27154=CARTESIAN_POINT('',(119.962847072938,230.,-29.3968363633866));
#27155=CARTESIAN_POINT('',(125.314401519217,230.,-34.5032237681315));
#27156=CARTESIAN_POINT('',(109.317622593617,230.,-34.5032237681315));
#27157=CARTESIAN_POINT('',(127.968500624638,230.,-37.1752157277839));
#27158=CARTESIAN_POINT('',(111.34106001963,230.,-20.435679696352));
#27159=CARTESIAN_POINT('',(128.273548427401,230.,-37.9151793916432));
#27160=CARTESIAN_POINT('Origin',(127.223548427401,230.,-37.9151793916432));
#27161=CARTESIAN_POINT('',(128.273548427401,230.,-39.4187321117283));
#27162=CARTESIAN_POINT('',(128.273548427401,230.,-18.9575896958216));
#27163=CARTESIAN_POINT('',(127.971127263844,230.,-40.1560420081102));
#27164=CARTESIAN_POINT('Origin',(127.223548427401,230.,-39.4187321117283));
#27165=CARTESIAN_POINT('',(127.333356762198,230.,-40.8026951072716));
#27166=CARTESIAN_POINT('',(132.044740758987,230.,-36.025692948968));
#27167=CARTESIAN_POINT('',(126.997701127708,230.,-41.3560806824536));
#27168=CARTESIAN_POINT('Origin',(128.330128544122,230.,-41.785774969114));
#27169=CARTESIAN_POINT('',(125.328762843953,230.,-42.9220241352404));
#27170=CARTESIAN_POINT('Origin',(124.747780443448,230.,-40.6305041508116));
#27171=CARTESIAN_POINT('',(124.876218876064,230.,-43.5036225521864));
#27172=CARTESIAN_POINT('Origin',(125.476218876064,230.,-43.5036225521863));
#27173=CARTESIAN_POINT('',(124.876218876064,230.,-44.4226470147914));
#27174=CARTESIAN_POINT('',(124.876218876064,230.,-21.751811276093));
#27175=CARTESIAN_POINT('',(125.387243744723,230.,-45.1153516005764));
#27176=CARTESIAN_POINT('Origin',(125.601218876064,230.,-44.4226470147914));
#27177=CARTESIAN_POINT('',(127.036092546462,230.,-46.8112703207193));
#27178=CARTESIAN_POINT('Origin',(124.659008759128,230.,-47.4728765656934));
#27179=CARTESIAN_POINT('',(127.149786002621,230.,-47.007169160326));
#27180=CARTESIAN_POINT('Origin',(127.469614165074,230.,-46.690609613792));
#27181=CARTESIAN_POINT('',(127.637659789347,230.,-47.5000804575095));
#27182=CARTESIAN_POINT('',(109.61588112148,230.,-29.2922190342974));
#27183=CARTESIAN_POINT('',(142.094409841973,230.,-47.5000804575095));
#27184=CARTESIAN_POINT('',(115.708222654194,230.,-47.5000804575095));
#27185=CARTESIAN_POINT('',(142.5822836287,230.,-47.007169160326));
#27186=CARTESIAN_POINT('',(144.48829315277,230.,-45.0814792533986));
#27187=CARTESIAN_POINT('',(142.695977084858,230.,-46.8112703207193));
#27188=CARTESIAN_POINT('Origin',(142.262455466246,230.,-46.690609613792));
#27189=CARTESIAN_POINT('',(144.344825886597,230.,-45.1153516005764));
#27190=CARTESIAN_POINT('Origin',(145.073060872192,230.,-47.4728765656934));
#27191=CARTESIAN_POINT('',(144.855850755256,230.,-44.4226470147914));
#27192=CARTESIAN_POINT('Origin',(144.130850755256,230.,-44.4226470147914));
#27193=CARTESIAN_POINT('',(144.855850755256,230.,-43.5036225521863));
#27194=CARTESIAN_POINT('',(144.855850755256,230.,-22.2113235073957));
#27195=CARTESIAN_POINT('',(144.403306787367,230.,-42.9220241352404));
#27196=CARTESIAN_POINT('Origin',(144.255850755256,230.,-43.5036225521863));
#27197=CARTESIAN_POINT('',(142.734368503612,230.,-41.3560806824536));
#27198=CARTESIAN_POINT('Origin',(144.984289187872,230.,-40.6305041508117));
#27199=CARTESIAN_POINT('',(142.398712869122,230.,-40.8026951072716));
#27200=CARTESIAN_POINT('Origin',(141.401941087198,230.,-41.7857749691141));
#27201=CARTESIAN_POINT('',(141.760942367476,230.,-40.1560420081102));
#27202=CARTESIAN_POINT('',(122.677567086127,230.,-20.8068815557118));
#27203=CARTESIAN_POINT('',(141.458521203919,230.,-39.4187321117283));
#27204=CARTESIAN_POINT('Origin',(142.508521203919,230.,-39.4187321117283));
#27205=CARTESIAN_POINT('',(141.458521203919,230.,-37.9151793916432));
#27206=CARTESIAN_POINT('',(141.45852120392,230.,-19.7093660558644));
#27207=CARTESIAN_POINT('',(141.763569006683,230.,-37.1752157277839));
#27208=CARTESIAN_POINT('Origin',(142.508521203919,230.,-37.9151793916432));
#27209=CARTESIAN_POINT('',(144.417668112103,230.,-34.5032237681314));
#27210=CARTESIAN_POINT('',(141.62477097808,230.,-37.3149494761148));
#27211=CARTESIAN_POINT('',(154.875609963127,230.,-34.5032237681314));
#27212=CARTESIAN_POINT('',(124.098226815572,230.,-34.5032237681314));
#27213=CARTESIAN_POINT('',(156.375609963127,230.,-36.0032237681314));
#27214=CARTESIAN_POINT('',(133.475597910073,230.,-13.1032117150771));
#27215=CARTESIAN_POINT('',(156.375609963127,230.,-58.0910625167936));
#27216=CARTESIAN_POINT('',(156.375609963127,230.,-18.0016118840657));
#27217=CARTESIAN_POINT('',(155.375609963127,230.,-59.0910625167936));
#27218=CARTESIAN_POINT('',(154.960007558403,230.,-59.5066649215182));
#27219=CARTESIAN_POINT('',(114.356459668193,230.,-59.0910625167936));
#27220=CARTESIAN_POINT('',(150.62266449878,230.,-59.0910625167936));
#27221=CARTESIAN_POINT('',(120.773904182304,230.,-65.5085070309049));
#27222=CARTESIAN_POINT('Origin',(142.094409841973,255.,-47.5000804575095));
#27223=CARTESIAN_POINT('',(142.094409841973,216.,-47.5000804575095));
#27224=CARTESIAN_POINT('',(142.094409841973,255.,-47.5000804575095));
#27225=CARTESIAN_POINT('',(142.5822836287,216.,-47.007169160326));
#27226=CARTESIAN_POINT('',(142.5822836287,216.,-47.007169160326));
#27227=CARTESIAN_POINT('',(142.5822836287,255.,-47.007169160326));
#27228=CARTESIAN_POINT('Origin',(142.262455466246,255.,-46.690609613792));
#27229=CARTESIAN_POINT('',(142.695977084858,216.,-46.8112703207193));
#27230=CARTESIAN_POINT('Origin',(142.262455466246,216.,-46.690609613792));
#27231=CARTESIAN_POINT('',(142.695977084858,255.,-46.8112703207193));
#27232=CARTESIAN_POINT('Origin',(145.073060872192,255.,-47.4728765656934));
#27233=CARTESIAN_POINT('',(144.344825886597,216.,-45.1153516005764));
#27234=CARTESIAN_POINT('Origin',(145.073060872192,216.,-47.4728765656934));
#27235=CARTESIAN_POINT('',(144.344825886597,255.,-45.1153516005764));
#27236=CARTESIAN_POINT('Origin',(144.130850755256,255.,-44.4226470147914));
#27237=CARTESIAN_POINT('',(144.855850755256,216.,-44.4226470147914));
#27238=CARTESIAN_POINT('Origin',(144.130850755256,216.,-44.4226470147914));
#27239=CARTESIAN_POINT('',(144.855850755256,255.,-44.4226470147914));
#27240=CARTESIAN_POINT('Origin',(144.855850755256,255.,-44.4226470147914));
#27241=CARTESIAN_POINT('',(144.855850755256,216.,-43.5036225521863));
#27242=CARTESIAN_POINT('',(144.855850755256,216.,-43.5036225521863));
#27243=CARTESIAN_POINT('',(144.855850755256,255.,-43.5036225521863));
#27244=CARTESIAN_POINT('Origin',(144.255850755256,255.,-43.5036225521863));
#27245=CARTESIAN_POINT('',(144.403306787367,216.,-42.9220241352404));
#27246=CARTESIAN_POINT('Origin',(144.255850755256,216.,-43.5036225521863));
#27247=CARTESIAN_POINT('',(144.403306787367,255.,-42.9220241352404));
#27248=CARTESIAN_POINT('Origin',(144.984289187872,255.,-40.6305041508117));
#27249=CARTESIAN_POINT('',(142.734368503612,216.,-41.3560806824536));
#27250=CARTESIAN_POINT('Origin',(144.984289187872,216.,-40.6305041508117));
#27251=CARTESIAN_POINT('',(142.734368503612,255.,-41.3560806824536));
#27252=CARTESIAN_POINT('Origin',(141.401941087198,255.,-41.7857749691141));
#27253=CARTESIAN_POINT('',(142.398712869122,216.,-40.8026951072716));
#27254=CARTESIAN_POINT('Origin',(141.401941087198,216.,-41.7857749691141));
#27255=CARTESIAN_POINT('',(142.398712869122,255.,-40.8026951072716));
#27256=CARTESIAN_POINT('Origin',(142.398712869122,255.,-40.8026951072716));
#27257=CARTESIAN_POINT('',(141.760942367476,216.,-40.1560420081102));
#27258=CARTESIAN_POINT('',(141.760942367476,216.,-40.1560420081102));
#27259=CARTESIAN_POINT('',(141.760942367476,255.,-40.1560420081102));
#27260=CARTESIAN_POINT('Origin',(142.508521203919,255.,-39.4187321117283));
#27261=CARTESIAN_POINT('',(141.458521203919,216.,-39.4187321117283));
#27262=CARTESIAN_POINT('Origin',(142.508521203919,216.,-39.4187321117283));
#27263=CARTESIAN_POINT('',(141.458521203919,255.,-39.4187321117283));
#27264=CARTESIAN_POINT('Origin',(141.458521203919,255.,-39.4187321117283));
#27265=CARTESIAN_POINT('',(141.458521203919,216.,-37.9151793916432));
#27266=CARTESIAN_POINT('',(141.458521203919,216.,-37.9151793916432));
#27267=CARTESIAN_POINT('',(141.458521203919,255.,-37.9151793916432));
#27268=CARTESIAN_POINT('Origin',(142.508521203919,255.,-37.9151793916432));
#27269=CARTESIAN_POINT('',(141.763569006683,216.,-37.1752157277839));
#27270=CARTESIAN_POINT('Origin',(142.508521203919,216.,-37.9151793916432));
#27271=CARTESIAN_POINT('',(141.763569006683,255.,-37.1752157277839));
#27272=CARTESIAN_POINT('Origin',(141.763569006683,255.,-37.1752157277839));
#27273=CARTESIAN_POINT('',(144.417668112103,216.,-34.5032237681314));
#27274=CARTESIAN_POINT('',(144.544688744748,216.,-34.375346814161));
#27275=CARTESIAN_POINT('',(144.417668112103,255.,-34.5032237681314));
#27276=CARTESIAN_POINT('Origin',(144.417668112103,255.,-34.5032237681314));
#27277=CARTESIAN_POINT('',(154.875609963127,216.,-34.5032237681314));
#27278=CARTESIAN_POINT('',(134.86603481566,216.,-34.5032237681314));
#27279=CARTESIAN_POINT('',(154.875609963127,255.,-34.5032237681314));
#27280=CARTESIAN_POINT('Origin',(154.875609963127,255.,-34.5032237681314));
#27281=CARTESIAN_POINT('',(156.375609963127,216.,-36.0032237681314));
#27282=CARTESIAN_POINT('',(154.875609963127,216.,-34.5032237681314));
#27283=CARTESIAN_POINT('',(156.375609963127,255.,-36.0032237681314));
#27284=CARTESIAN_POINT('Origin',(156.375609963127,255.,-36.0032237681314));
#27285=CARTESIAN_POINT('',(156.375609963127,216.,-58.0910625167936));
#27286=CARTESIAN_POINT('',(156.375609963127,216.,-36.0032237681314));
#27287=CARTESIAN_POINT('',(156.375609963127,255.,-58.0910625167936));
#27288=CARTESIAN_POINT('Origin',(113.356459668193,255.,-58.0910625167937));
#27289=CARTESIAN_POINT('',(113.356459668193,216.,-58.0910625167937));
#27290=CARTESIAN_POINT('',(113.356459668193,255.,-58.0910625167937));
#27291=CARTESIAN_POINT('',(113.356459668193,216.,-36.0032237681315));
#27292=CARTESIAN_POINT('',(113.356459668193,216.,-36.0032237681315));
#27293=CARTESIAN_POINT('',(113.356459668193,255.,-36.0032237681315));
#27294=CARTESIAN_POINT('Origin',(113.356459668193,255.,-36.0032237681315));
#27295=CARTESIAN_POINT('',(114.856459668193,216.,-34.5032237681315));
#27296=CARTESIAN_POINT('',(114.856459668193,216.,-34.5032237681315));
#27297=CARTESIAN_POINT('',(114.856459668193,255.,-34.5032237681315));
#27298=CARTESIAN_POINT('Origin',(114.856459668193,255.,-34.5032237681315));
#27299=CARTESIAN_POINT('',(125.314401519217,216.,-34.5032237681315));
#27300=CARTESIAN_POINT('',(134.86603481566,216.,-34.5032237681314));
#27301=CARTESIAN_POINT('',(125.314401519217,255.,-34.5032237681315));
#27302=CARTESIAN_POINT('Origin',(125.314401519217,255.,-34.5032237681315));
#27303=CARTESIAN_POINT('',(127.968500624638,216.,-37.1752157277839));
#27304=CARTESIAN_POINT('',(127.968500624638,216.,-37.1752157277839));
#27305=CARTESIAN_POINT('',(127.968500624638,255.,-37.1752157277839));
#27306=CARTESIAN_POINT('Origin',(127.223548427401,255.,-37.9151793916432));
#27307=CARTESIAN_POINT('',(128.273548427401,216.,-37.9151793916432));
#27308=CARTESIAN_POINT('Origin',(127.223548427401,216.,-37.9151793916432));
#27309=CARTESIAN_POINT('',(128.273548427401,255.,-37.9151793916432));
#27310=CARTESIAN_POINT('Origin',(156.375609963127,255.,-58.0910625167936));
#27311=CARTESIAN_POINT('',(155.375609963127,216.,-59.0910625167936));
#27312=CARTESIAN_POINT('',(156.375609963127,216.,-58.0910625167936));
#27313=CARTESIAN_POINT('',(155.375609963127,255.,-59.0910625167936));
#27314=CARTESIAN_POINT('Origin',(155.375609963127,255.,-59.0910625167936));
#27315=CARTESIAN_POINT('',(114.356459668193,216.,-59.0910625167936));
#27316=CARTESIAN_POINT('',(155.375609963127,216.,-59.0910625167936));
#27317=CARTESIAN_POINT('',(114.356459668193,255.,-59.0910625167936));
#27318=CARTESIAN_POINT('Origin',(114.356459668193,255.,-59.0910625167936));
#27319=CARTESIAN_POINT('',(113.356459668193,216.,-58.0910625167937));
#27320=CARTESIAN_POINT('Origin',(128.273548427401,255.,-37.9151793916432));
#27321=CARTESIAN_POINT('',(128.273548427401,216.,-39.4187321117283));
#27322=CARTESIAN_POINT('',(128.273548427401,216.,-39.4187321117283));
#27323=CARTESIAN_POINT('',(128.273548427401,255.,-39.4187321117283));
#27324=CARTESIAN_POINT('Origin',(127.637659789347,255.,-47.5000804575095));
#27325=CARTESIAN_POINT('',(127.637659789347,216.,-47.5000804575095));
#27326=CARTESIAN_POINT('',(127.637659789347,255.,-47.5000804575095));
#27327=CARTESIAN_POINT('',(142.094409841973,216.,-47.5000804575095));
#27328=CARTESIAN_POINT('Origin',(127.149786002621,255.,-47.007169160326));
#27329=CARTESIAN_POINT('',(127.149786002621,216.,-47.007169160326));
#27330=CARTESIAN_POINT('',(127.149786002621,255.,-47.007169160326));
#27331=CARTESIAN_POINT('',(127.637659789347,216.,-47.5000804575095));
#27332=CARTESIAN_POINT('Origin',(127.469614165074,255.,-46.690609613792));
#27333=CARTESIAN_POINT('',(127.036092546462,216.,-46.8112703207193));
#27334=CARTESIAN_POINT('',(127.036092546462,255.,-46.8112703207193));
#27335=CARTESIAN_POINT('Origin',(127.469614165074,216.,-46.690609613792));
#27336=CARTESIAN_POINT('Origin',(124.659008759128,255.,-47.4728765656934));
#27337=CARTESIAN_POINT('',(125.387243744723,216.,-45.1153516005764));
#27338=CARTESIAN_POINT('',(125.387243744723,255.,-45.1153516005764));
#27339=CARTESIAN_POINT('Origin',(124.659008759128,216.,-47.4728765656934));
#27340=CARTESIAN_POINT('Origin',(125.601218876064,255.,-44.4226470147914));
#27341=CARTESIAN_POINT('',(124.876218876064,216.,-44.4226470147914));
#27342=CARTESIAN_POINT('',(124.876218876064,255.,-44.4226470147914));
#27343=CARTESIAN_POINT('Origin',(125.601218876064,216.,-44.4226470147914));
#27344=CARTESIAN_POINT('Origin',(124.876218876064,255.,-43.5036225521864));
#27345=CARTESIAN_POINT('',(124.876218876064,216.,-43.5036225521864));
#27346=CARTESIAN_POINT('',(124.876218876064,255.,-43.5036225521864));
#27347=CARTESIAN_POINT('',(124.876218876064,216.,-44.4226470147914));
#27348=CARTESIAN_POINT('Origin',(125.476218876064,255.,-43.5036225521863));
#27349=CARTESIAN_POINT('',(125.328762843953,216.,-42.9220241352404));
#27350=CARTESIAN_POINT('',(125.328762843953,255.,-42.9220241352404));
#27351=CARTESIAN_POINT('Origin',(125.476218876064,216.,-43.5036225521863));
#27352=CARTESIAN_POINT('Origin',(124.747780443448,255.,-40.6305041508116));
#27353=CARTESIAN_POINT('',(126.997701127708,216.,-41.3560806824536));
#27354=CARTESIAN_POINT('',(126.997701127708,255.,-41.3560806824536));
#27355=CARTESIAN_POINT('Origin',(124.747780443448,216.,-40.6305041508116));
#27356=CARTESIAN_POINT('Origin',(128.330128544122,255.,-41.785774969114));
#27357=CARTESIAN_POINT('',(127.333356762198,216.,-40.8026951072716));
#27358=CARTESIAN_POINT('',(127.333356762198,255.,-40.8026951072716));
#27359=CARTESIAN_POINT('Origin',(128.330128544122,216.,-41.785774969114));
#27360=CARTESIAN_POINT('Origin',(127.971127263844,255.,-40.1560420081102));
#27361=CARTESIAN_POINT('',(127.971127263844,216.,-40.1560420081102));
#27362=CARTESIAN_POINT('',(127.971127263844,255.,-40.1560420081102));
#27363=CARTESIAN_POINT('',(127.333356762198,216.,-40.8026951072716));
#27364=CARTESIAN_POINT('Origin',(127.223548427401,255.,-39.4187321117283));
#27365=CARTESIAN_POINT('Origin',(127.223548427401,216.,-39.4187321117283));
#27366=CARTESIAN_POINT('Origin',(134.86603481566,216.,-46.7971431424625));
#27367=CARTESIAN_POINT('Origin',(142.094409841973,255.,-47.5000804575095));
#27368=CARTESIAN_POINT('',(142.094409841973,230.,-47.5000804575095));
#27369=CARTESIAN_POINT('',(142.5822836287,230.,-47.007169160326));
#27370=CARTESIAN_POINT('',(144.48829315277,230.,-45.0814792533986));
#27371=CARTESIAN_POINT('',(142.5822836287,280.,-47.007169160326));
#27372=CARTESIAN_POINT('',(142.5822836287,255.,-47.007169160326));
#27373=CARTESIAN_POINT('',(142.094409841973,280.,-47.5000804575095));
#27374=CARTESIAN_POINT('',(144.655606318974,280.,-44.9124385054979));
#27375=CARTESIAN_POINT('',(142.094409841973,255.,-47.5000804575095));
#27376=CARTESIAN_POINT('Origin',(142.262455466246,255.,-46.690609613792));
#27377=CARTESIAN_POINT('',(142.695977084858,230.,-46.8112703207193));
#27378=CARTESIAN_POINT('Origin',(142.262455466246,230.,-46.690609613792));
#27379=CARTESIAN_POINT('',(142.695977084858,280.,-46.8112703207193));
#27380=CARTESIAN_POINT('',(142.695977084858,255.,-46.8112703207193));
#27381=CARTESIAN_POINT('Origin',(142.262455466246,280.,-46.690609613792));
#27382=CARTESIAN_POINT('Origin',(145.073060872192,255.,-47.4728765656934));
#27383=CARTESIAN_POINT('',(144.344825886597,230.,-45.1153516005764));
#27384=CARTESIAN_POINT('Origin',(145.073060872192,230.,-47.4728765656934));
#27385=CARTESIAN_POINT('',(144.344825886597,280.,-45.1153516005764));
#27386=CARTESIAN_POINT('',(144.344825886597,255.,-45.1153516005764));
#27387=CARTESIAN_POINT('Origin',(145.073060872192,280.,-47.4728765656934));
#27388=CARTESIAN_POINT('Origin',(144.130850755256,255.,-44.4226470147914));
#27389=CARTESIAN_POINT('',(144.855850755256,230.,-44.4226470147914));
#27390=CARTESIAN_POINT('Origin',(144.130850755256,230.,-44.4226470147914));
#27391=CARTESIAN_POINT('',(144.855850755256,280.,-44.4226470147914));
#27392=CARTESIAN_POINT('',(144.855850755256,255.,-44.4226470147914));
#27393=CARTESIAN_POINT('Origin',(144.130850755256,280.,-44.4226470147914));
#27394=CARTESIAN_POINT('Origin',(144.855850755256,255.,-44.4226470147914));
#27395=CARTESIAN_POINT('',(144.855850755256,230.,-43.5036225521863));
#27396=CARTESIAN_POINT('',(144.855850755256,230.,-22.2113235073957));
#27397=CARTESIAN_POINT('',(144.855850755256,280.,-43.5036225521863));
#27398=CARTESIAN_POINT('',(144.855850755256,255.,-43.5036225521863));
#27399=CARTESIAN_POINT('',(144.855850755256,280.,-22.2113235073957));
#27400=CARTESIAN_POINT('Origin',(144.255850755256,255.,-43.5036225521863));
#27401=CARTESIAN_POINT('',(144.403306787367,230.,-42.9220241352404));
#27402=CARTESIAN_POINT('Origin',(144.255850755256,230.,-43.5036225521863));
#27403=CARTESIAN_POINT('',(144.403306787367,280.,-42.9220241352404));
#27404=CARTESIAN_POINT('',(144.403306787367,255.,-42.9220241352404));
#27405=CARTESIAN_POINT('Origin',(144.255850755256,280.,-43.5036225521863));
#27406=CARTESIAN_POINT('Origin',(144.984289187872,255.,-40.6305041508117));
#27407=CARTESIAN_POINT('',(142.734368503612,230.,-41.3560806824536));
#27408=CARTESIAN_POINT('Origin',(144.984289187872,230.,-40.6305041508117));
#27409=CARTESIAN_POINT('',(142.734368503612,280.,-41.3560806824536));
#27410=CARTESIAN_POINT('',(142.734368503612,255.,-41.3560806824536));
#27411=CARTESIAN_POINT('Origin',(144.984289187872,280.,-40.6305041508117));
#27412=CARTESIAN_POINT('Origin',(145.869719034433,230.,-53.247581206998));
#27413=CARTESIAN_POINT('',(156.375609963127,230.,-46.4955106076453));
#27414=CARTESIAN_POINT('',(156.873403253207,230.,-46.9933038977248));
#27415=CARTESIAN_POINT('',(156.373403253207,230.,-46.4933038977248));
#27416=CARTESIAN_POINT('',(156.375609963127,230.,-36.0032237681314));
#27417=CARTESIAN_POINT('',(156.375609963127,230.,-18.0016118840657));
#27418=CARTESIAN_POINT('',(154.875609963127,230.,-34.5032237681314));
#27419=CARTESIAN_POINT('',(133.475597910073,230.,-13.1032117150771));
#27420=CARTESIAN_POINT('',(144.417668112103,230.,-34.5032237681314));
#27421=CARTESIAN_POINT('',(124.098226815572,230.,-34.5032237681314));
#27422=CARTESIAN_POINT('',(141.763569006683,230.,-37.1752157277839));
#27423=CARTESIAN_POINT('',(141.62477097808,230.,-37.3149494761148));
#27424=CARTESIAN_POINT('',(141.458521203919,230.,-37.9151793916432));
#27425=CARTESIAN_POINT('Origin',(142.508521203919,230.,-37.9151793916432));
#27426=CARTESIAN_POINT('',(141.458521203919,230.,-39.4187321117283));
#27427=CARTESIAN_POINT('',(141.45852120392,230.,-19.7093660558644));
#27428=CARTESIAN_POINT('',(141.760942367476,230.,-40.1560420081102));
#27429=CARTESIAN_POINT('Origin',(142.508521203919,230.,-39.4187321117283));
#27430=CARTESIAN_POINT('',(142.398712869122,230.,-40.8026951072716));
#27431=CARTESIAN_POINT('',(122.677567086127,230.,-20.8068815557118));
#27432=CARTESIAN_POINT('Origin',(141.401941087198,230.,-41.7857749691141));
#27433=CARTESIAN_POINT('',(127.637659789347,230.,-47.5000804575095));
#27434=CARTESIAN_POINT('',(115.708222654194,230.,-47.5000804575095));
#27435=CARTESIAN_POINT('',(127.149786002621,230.,-47.007169160326));
#27436=CARTESIAN_POINT('',(109.61588112148,230.,-29.2922190342974));
#27437=CARTESIAN_POINT('',(127.036092546462,230.,-46.8112703207193));
#27438=CARTESIAN_POINT('Origin',(127.469614165074,230.,-46.690609613792));
#27439=CARTESIAN_POINT('',(125.387243744723,230.,-45.1153516005764));
#27440=CARTESIAN_POINT('Origin',(124.659008759128,230.,-47.4728765656934));
#27441=CARTESIAN_POINT('',(124.876218876064,230.,-44.4226470147914));
#27442=CARTESIAN_POINT('Origin',(125.601218876064,230.,-44.4226470147914));
#27443=CARTESIAN_POINT('',(124.876218876064,230.,-43.5036225521864));
#27444=CARTESIAN_POINT('',(124.876218876064,230.,-21.751811276093));
#27445=CARTESIAN_POINT('',(125.328762843953,230.,-42.9220241352404));
#27446=CARTESIAN_POINT('Origin',(125.476218876064,230.,-43.5036225521863));
#27447=CARTESIAN_POINT('',(126.997701127708,230.,-41.3560806824536));
#27448=CARTESIAN_POINT('Origin',(124.747780443448,230.,-40.6305041508116));
#27449=CARTESIAN_POINT('',(127.333356762198,230.,-40.8026951072716));
#27450=CARTESIAN_POINT('Origin',(128.330128544122,230.,-41.785774969114));
#27451=CARTESIAN_POINT('',(127.971127263844,230.,-40.1560420081102));
#27452=CARTESIAN_POINT('',(132.044740758987,230.,-36.025692948968));
#27453=CARTESIAN_POINT('',(128.273548427401,230.,-39.4187321117283));
#27454=CARTESIAN_POINT('Origin',(127.223548427401,230.,-39.4187321117283));
#27455=CARTESIAN_POINT('',(128.273548427401,230.,-37.9151793916432));
#27456=CARTESIAN_POINT('',(128.273548427401,230.,-18.9575896958216));
#27457=CARTESIAN_POINT('',(127.968500624638,230.,-37.1752157277839));
#27458=CARTESIAN_POINT('Origin',(127.223548427401,230.,-37.9151793916432));
#27459=CARTESIAN_POINT('',(125.314401519217,230.,-34.5032237681315));
#27460=CARTESIAN_POINT('',(111.34106001963,230.,-20.435679696352));
#27461=CARTESIAN_POINT('',(114.856459668193,230.,-34.5032237681315));
#27462=CARTESIAN_POINT('',(109.317622593617,230.,-34.5032237681315));
#27463=CARTESIAN_POINT('',(113.356459668193,230.,-36.0032237681315));
#27464=CARTESIAN_POINT('',(119.962847072938,230.,-29.3968363633866));
#27465=CARTESIAN_POINT('',(113.356459668193,230.,-46.4955106076453));
#27466=CARTESIAN_POINT('',(113.356459668193,230.,-29.0455312583968));
#27467=CARTESIAN_POINT('',(112.858666378114,230.,-46.9933038977248));
#27468=CARTESIAN_POINT('',(113.358666378114,230.,-46.4933038977248));
#27469=CARTESIAN_POINT('',(112.858666378113,230.,-58.9996518063507));
#27470=CARTESIAN_POINT('',(112.858666378114,230.,-46.9933038977248));
#27471=CARTESIAN_POINT('',(113.858666378113,230.,-59.9996518063507));
#27472=CARTESIAN_POINT('',(112.858666378113,230.,-58.9996518063507));
#27473=CARTESIAN_POINT('',(122.862905683347,230.,-59.9996518063507));
#27474=CARTESIAN_POINT('',(113.858666378113,230.,-59.9996518063507));
#27475=CARTESIAN_POINT('',(124.265819387872,230.,-59.4840979918677));
#27476=CARTESIAN_POINT('Origin',(124.265819387872,230.,-61.6506638626042));
#27477=CARTESIAN_POINT('',(145.466250243448,230.,-59.4840979918677));
#27478=CARTESIAN_POINT('',(145.466250243448,230.,-59.4840979918677));
#27479=CARTESIAN_POINT('',(146.869163947974,230.,-59.9996518063508));
#27480=CARTESIAN_POINT('Origin',(145.466250243448,230.,-61.6506638626042));
#27481=CARTESIAN_POINT('',(155.873403253207,230.,-59.9996518063507));
#27482=CARTESIAN_POINT('',(155.873403253207,230.,-59.9996518063507));
#27483=CARTESIAN_POINT('',(156.873403253207,230.,-58.9996518063507));
#27484=CARTESIAN_POINT('',(156.873403253207,230.,-58.9996518063507));
#27485=CARTESIAN_POINT('',(156.873403253207,230.,-46.9933038977248));
#27486=CARTESIAN_POINT('Origin',(156.375609963127,255.,-46.4955106076453));
#27487=CARTESIAN_POINT('',(156.873403253207,280.,-46.9933038977248));
#27488=CARTESIAN_POINT('',(156.873403253207,255.,-46.9933038977248));
#27489=CARTESIAN_POINT('',(156.375609963127,280.,-46.4955106076453));
#27490=CARTESIAN_POINT('',(156.373403253207,280.,-46.4933038977248));
#27491=CARTESIAN_POINT('',(156.375609963127,255.,-46.4955106076453));
#27492=CARTESIAN_POINT('Origin',(156.873403253207,255.,-46.9933038977248));
#27493=CARTESIAN_POINT('',(156.873403253207,280.,-58.9996518063507));
#27494=CARTESIAN_POINT('',(156.873403253207,255.,-58.9996518063507));
#27495=CARTESIAN_POINT('',(156.873403253207,280.,-46.9933038977248));
#27496=CARTESIAN_POINT('Origin',(156.873403253207,255.,-58.9996518063507));
#27497=CARTESIAN_POINT('',(155.873403253207,280.,-59.9996518063507));
#27498=CARTESIAN_POINT('',(155.873403253207,255.,-59.9996518063507));
#27499=CARTESIAN_POINT('',(156.873403253207,280.,-58.9996518063507));
#27500=CARTESIAN_POINT('Origin',(155.873403253207,255.,-59.9996518063507));
#27501=CARTESIAN_POINT('',(146.869163947974,280.,-59.9996518063508));
#27502=CARTESIAN_POINT('',(146.869163947974,255.,-59.9996518063508));
#27503=CARTESIAN_POINT('',(155.873403253207,280.,-59.9996518063507));
#27504=CARTESIAN_POINT('',(154.37128360059,270.562970493524,-59.9996518063507));
#27505=CARTESIAN_POINT('Origin',(151.37128360059,270.562970493524,-59.9996518063507));
#27506=CARTESIAN_POINT('',(154.37128360059,238.562970493524,-59.9996518063507));
#27507=CARTESIAN_POINT('Origin',(151.37128360059,238.562970493524,-59.9996518063507));
#27508=CARTESIAN_POINT('Origin',(145.466250243448,255.,-61.6506638626042));
#27509=CARTESIAN_POINT('',(145.466250243448,280.,-59.4840979918677));
#27510=CARTESIAN_POINT('',(145.466250243448,255.,-59.4840979918677));
#27511=CARTESIAN_POINT('Origin',(145.466250243448,280.,-61.6506638626042));
#27512=CARTESIAN_POINT('Origin',(145.466250243448,255.,-59.4840979918677));
#27513=CARTESIAN_POINT('',(124.265819387872,280.,-59.4840979918677));
#27514=CARTESIAN_POINT('',(124.265819387872,255.,-59.4840979918677));
#27515=CARTESIAN_POINT('',(124.265819387872,280.,-59.4840979918677));
#27516=CARTESIAN_POINT('Origin',(145.869719034433,280.,-53.247581206998));
#27517=CARTESIAN_POINT('',(122.862905683347,280.,-59.9996518063507));
#27518=CARTESIAN_POINT('Origin',(124.265819387872,280.,-61.6506638626042));
#27519=CARTESIAN_POINT('',(113.858666378113,280.,-59.9996518063507));
#27520=CARTESIAN_POINT('',(113.858666378113,280.,-59.9996518063507));
#27521=CARTESIAN_POINT('',(112.858666378113,280.,-58.9996518063507));
#27522=CARTESIAN_POINT('',(112.858666378113,280.,-58.9996518063507));
#27523=CARTESIAN_POINT('',(112.858666378114,280.,-46.9933038977248));
#27524=CARTESIAN_POINT('',(112.858666378114,280.,-46.9933038977248));
#27525=CARTESIAN_POINT('',(113.356459668193,280.,-46.4955106076453));
#27526=CARTESIAN_POINT('',(113.358666378114,280.,-46.4933038977248));
#27527=CARTESIAN_POINT('',(113.356459668193,280.,-36.0032237681315));
#27528=CARTESIAN_POINT('',(113.356459668193,280.,-29.0455312583968));
#27529=CARTESIAN_POINT('',(114.856459668193,280.,-34.5032237681315));
#27530=CARTESIAN_POINT('',(120.131896739857,280.,-29.2277866964671));
#27531=CARTESIAN_POINT('',(125.314401519217,280.,-34.5032237681315));
#27532=CARTESIAN_POINT('',(109.655721927456,280.,-34.5032237681315));
#27533=CARTESIAN_POINT('',(127.968500624638,280.,-37.1752157277839));
#27534=CARTESIAN_POINT('',(111.508973864096,280.,-20.6047255475076));
#27535=CARTESIAN_POINT('',(128.273548427401,280.,-37.9151793916432));
#27536=CARTESIAN_POINT('Origin',(127.223548427401,280.,-37.9151793916432));
#27537=CARTESIAN_POINT('',(128.273548427401,280.,-39.4187321117283));
#27538=CARTESIAN_POINT('',(128.273548427401,280.,-18.9575896958216));
#27539=CARTESIAN_POINT('',(127.971127263844,280.,-40.1560420081102));
#27540=CARTESIAN_POINT('Origin',(127.223548427401,280.,-39.4187321117283));
#27541=CARTESIAN_POINT('',(127.333356762198,280.,-40.8026951072716));
#27542=CARTESIAN_POINT('',(132.211452368059,280.,-35.85665945119));
#27543=CARTESIAN_POINT('',(126.997701127708,280.,-41.3560806824536));
#27544=CARTESIAN_POINT('Origin',(128.330128544122,280.,-41.785774969114));
#27545=CARTESIAN_POINT('',(125.328762843953,280.,-42.9220241352404));
#27546=CARTESIAN_POINT('Origin',(124.747780443448,280.,-40.6305041508116));
#27547=CARTESIAN_POINT('',(124.876218876064,280.,-43.5036225521864));
#27548=CARTESIAN_POINT('Origin',(125.476218876064,280.,-43.5036225521863));
#27549=CARTESIAN_POINT('',(124.876218876064,280.,-44.4226470147914));
#27550=CARTESIAN_POINT('',(124.876218876064,280.,-21.751811276093));
#27551=CARTESIAN_POINT('',(125.387243744723,280.,-45.1153516005764));
#27552=CARTESIAN_POINT('Origin',(125.601218876064,280.,-44.4226470147914));
#27553=CARTESIAN_POINT('',(127.036092546462,280.,-46.8112703207193));
#27554=CARTESIAN_POINT('Origin',(124.659008759128,280.,-47.4728765656934));
#27555=CARTESIAN_POINT('',(127.149786002621,280.,-47.007169160326));
#27556=CARTESIAN_POINT('Origin',(127.469614165074,280.,-46.690609613792));
#27557=CARTESIAN_POINT('',(127.637659789347,280.,-47.5000804575095));
#27558=CARTESIAN_POINT('',(109.783194287684,280.,-29.4612597821981));
#27559=CARTESIAN_POINT('',(116.046321988033,280.,-47.5000804575095));
#27560=CARTESIAN_POINT('',(142.398712869122,280.,-40.8026951072716));
#27561=CARTESIAN_POINT('Origin',(141.401941087198,280.,-41.7857749691141));
#27562=CARTESIAN_POINT('',(141.760942367476,280.,-40.1560420081102));
#27563=CARTESIAN_POINT('',(122.844278695199,280.,-20.9759150534898));
#27564=CARTESIAN_POINT('',(141.458521203919,280.,-39.4187321117283));
#27565=CARTESIAN_POINT('Origin',(142.508521203919,280.,-39.4187321117283));
#27566=CARTESIAN_POINT('',(141.458521203919,280.,-37.9151793916432));
#27567=CARTESIAN_POINT('',(141.45852120392,280.,-19.7093660558643));
#27568=CARTESIAN_POINT('',(141.763569006683,280.,-37.1752157277839));
#27569=CARTESIAN_POINT('Origin',(142.508521203919,280.,-37.9151793916432));
#27570=CARTESIAN_POINT('',(144.417668112103,280.,-34.5032237681314));
#27571=CARTESIAN_POINT('',(141.792684822546,280.,-37.1459036249592));
#27572=CARTESIAN_POINT('',(154.875609963127,280.,-34.5032237681314));
#27573=CARTESIAN_POINT('',(124.436326149411,280.,-34.5032237681314));
#27574=CARTESIAN_POINT('',(156.375609963127,280.,-36.0032237681314));
#27575=CARTESIAN_POINT('',(133.644647576992,280.,-13.2722613819965));
#27576=CARTESIAN_POINT('',(156.375609963127,280.,-18.0016118840657));
#27577=CARTESIAN_POINT('Origin',(113.356459668193,255.,-46.4955106076453));
#27578=CARTESIAN_POINT('',(112.858666378114,255.,-46.9933038977248));
#27579=CARTESIAN_POINT('',(113.356459668193,255.,-46.4955106076453));
#27580=CARTESIAN_POINT('Origin',(112.858666378114,255.,-46.9933038977248));
#27581=CARTESIAN_POINT('',(112.858666378113,255.,-58.9996518063507));
#27582=CARTESIAN_POINT('Origin',(112.858666378113,255.,-58.9996518063507));
#27583=CARTESIAN_POINT('',(113.858666378113,255.,-59.9996518063507));
#27584=CARTESIAN_POINT('Origin',(113.858666378113,255.,-59.9996518063507));
#27585=CARTESIAN_POINT('',(122.862905683347,255.,-59.9996518063507));
#27586=CARTESIAN_POINT('',(121.37128360059,270.562970493524,-59.9996518063507));
#27587=CARTESIAN_POINT('Origin',(118.37128360059,270.562970493524,-59.9996518063507));
#27588=CARTESIAN_POINT('',(121.37128360059,238.562970493524,-59.9996518063507));
#27589=CARTESIAN_POINT('Origin',(118.37128360059,238.562970493524,-59.9996518063507));
#27590=CARTESIAN_POINT('Origin',(124.265819387872,255.,-61.6506638626042));
#27591=CARTESIAN_POINT('Origin',(151.37128360059,238.562970493524,-59.9996518063507));
#27592=CARTESIAN_POINT('',(154.37128360059,238.562970493524,-34.5032237681314));
#27593=CARTESIAN_POINT('',(154.37128360059,238.562970493524,-59.9996518063507));
#27594=CARTESIAN_POINT('Origin',(151.37128360059,238.562970493524,-34.5032237681314));
#27595=CARTESIAN_POINT('Origin',(118.37128360059,238.562970493524,-59.9996518063507));
#27596=CARTESIAN_POINT('',(121.37128360059,238.562970493524,-34.5032237681315));
#27597=CARTESIAN_POINT('',(121.37128360059,238.562970493524,-59.9996518063507));
#27598=CARTESIAN_POINT('Origin',(118.37128360059,238.562970493524,-34.5032237681315));
#27599=CARTESIAN_POINT('Origin',(151.37128360059,270.562970493524,-59.9996518063507));
#27600=CARTESIAN_POINT('',(154.37128360059,270.562970493524,-34.5032237681314));
#27601=CARTESIAN_POINT('',(154.37128360059,270.562970493524,-59.9996518063507));
#27602=CARTESIAN_POINT('Origin',(151.37128360059,270.562970493524,-34.5032237681314));
#27603=CARTESIAN_POINT('Origin',(118.37128360059,270.562970493524,-59.9996518063507));
#27604=CARTESIAN_POINT('',(121.37128360059,270.562970493524,-34.5032237681315));
#27605=CARTESIAN_POINT('',(121.37128360059,270.562970493524,-59.9996518063507));
#27606=CARTESIAN_POINT('Origin',(118.37128360059,270.562970493524,-34.5032237681315));
#27607=CARTESIAN_POINT('Origin',(156.375609963127,255.,-36.0032237681314));
#27608=CARTESIAN_POINT('',(156.375609963127,255.,-36.0032237681314));
#27609=CARTESIAN_POINT('Origin',(154.875609963127,255.,-34.5032237681314));
#27610=CARTESIAN_POINT('',(154.875609963127,255.,-34.5032237681314));
#27611=CARTESIAN_POINT('Origin',(144.417668112103,255.,-34.5032237681314));
#27612=CARTESIAN_POINT('',(144.417668112103,255.,-34.5032237681314));
#27613=CARTESIAN_POINT('Origin',(141.763569006683,255.,-37.1752157277839));
#27614=CARTESIAN_POINT('',(141.763569006683,255.,-37.1752157277839));
#27615=CARTESIAN_POINT('Origin',(142.508521203919,255.,-37.9151793916432));
#27616=CARTESIAN_POINT('',(141.458521203919,255.,-37.9151793916432));
#27617=CARTESIAN_POINT('Origin',(141.458521203919,255.,-39.4187321117283));
#27618=CARTESIAN_POINT('',(141.458521203919,255.,-39.4187321117283));
#27619=CARTESIAN_POINT('Origin',(142.508521203919,255.,-39.4187321117283));
#27620=CARTESIAN_POINT('',(141.760942367476,255.,-40.1560420081102));
#27621=CARTESIAN_POINT('Origin',(142.398712869122,255.,-40.8026951072716));
#27622=CARTESIAN_POINT('',(142.398712869122,255.,-40.8026951072716));
#27623=CARTESIAN_POINT('Origin',(141.401941087198,255.,-41.7857749691141));
#27624=CARTESIAN_POINT('Origin',(113.356459668193,255.,-58.0910625167937));
#27625=CARTESIAN_POINT('',(113.356459668193,255.,-36.0032237681315));
#27626=CARTESIAN_POINT('Origin',(113.356459668193,255.,-36.0032237681315));
#27627=CARTESIAN_POINT('',(114.856459668193,255.,-34.5032237681315));
#27628=CARTESIAN_POINT('Origin',(114.856459668193,255.,-34.5032237681315));
#27629=CARTESIAN_POINT('',(125.314401519217,255.,-34.5032237681315));
#27630=CARTESIAN_POINT('Origin',(125.314401519217,255.,-34.5032237681315));
#27631=CARTESIAN_POINT('',(127.968500624638,255.,-37.1752157277839));
#27632=CARTESIAN_POINT('Origin',(127.223548427401,255.,-37.9151793916432));
#27633=CARTESIAN_POINT('',(128.273548427401,255.,-37.9151793916432));
#27634=CARTESIAN_POINT('Origin',(128.273548427401,255.,-37.9151793916432));
#27635=CARTESIAN_POINT('',(128.273548427401,255.,-39.4187321117283));
#27636=CARTESIAN_POINT('Origin',(127.223548427401,255.,-39.4187321117283));
#27637=CARTESIAN_POINT('',(127.971127263844,255.,-40.1560420081102));
#27638=CARTESIAN_POINT('Origin',(127.971127263844,255.,-40.1560420081102));
#27639=CARTESIAN_POINT('',(127.333356762198,255.,-40.8026951072716));
#27640=CARTESIAN_POINT('Origin',(128.330128544122,255.,-41.785774969114));
#27641=CARTESIAN_POINT('',(126.997701127708,255.,-41.3560806824536));
#27642=CARTESIAN_POINT('Origin',(124.747780443448,255.,-40.6305041508116));
#27643=CARTESIAN_POINT('',(125.328762843953,255.,-42.9220241352404));
#27644=CARTESIAN_POINT('Origin',(125.476218876064,255.,-43.5036225521863));
#27645=CARTESIAN_POINT('',(124.876218876064,255.,-43.5036225521864));
#27646=CARTESIAN_POINT('Origin',(124.876218876064,255.,-43.5036225521864));
#27647=CARTESIAN_POINT('',(124.876218876064,255.,-44.4226470147914));
#27648=CARTESIAN_POINT('Origin',(125.601218876064,255.,-44.4226470147914));
#27649=CARTESIAN_POINT('',(125.387243744723,255.,-45.1153516005764));
#27650=CARTESIAN_POINT('Origin',(124.659008759128,255.,-47.4728765656934));
#27651=CARTESIAN_POINT('',(127.036092546462,255.,-46.8112703207193));
#27652=CARTESIAN_POINT('Origin',(127.469614165074,255.,-46.690609613792));
#27653=CARTESIAN_POINT('',(127.149786002621,255.,-47.007169160326));
#27654=CARTESIAN_POINT('Origin',(127.149786002621,255.,-47.007169160326));
#27655=CARTESIAN_POINT('',(127.637659789347,255.,-47.5000804575095));
#27656=CARTESIAN_POINT('Origin',(127.637659789347,255.,-47.5000804575095));
#27657=CARTESIAN_POINT('Origin',(141.401941087198,255.,-41.7857749691141));
#27658=CARTESIAN_POINT('',(142.734368503612,280.,-41.3560806824536));
#27659=CARTESIAN_POINT('',(142.398712869122,280.,-40.8026951072716));
#27660=CARTESIAN_POINT('Origin',(141.401941087198,280.,-41.7857749691141));
#27661=CARTESIAN_POINT('',(142.398712869122,294.,-40.8026951072716));
#27662=CARTESIAN_POINT('',(142.398712869122,255.,-40.8026951072716));
#27663=CARTESIAN_POINT('',(142.734368503612,294.,-41.3560806824536));
#27664=CARTESIAN_POINT('Origin',(141.401941087198,294.,-41.7857749691141));
#27665=CARTESIAN_POINT('',(142.734368503612,255.,-41.3560806824536));
#27666=CARTESIAN_POINT('Origin',(142.398712869122,255.,-40.8026951072716));
#27667=CARTESIAN_POINT('',(141.760942367476,280.,-40.1560420081102));
#27668=CARTESIAN_POINT('',(122.844278695199,280.,-20.9759150534898));
#27669=CARTESIAN_POINT('',(141.760942367476,294.,-40.1560420081102));
#27670=CARTESIAN_POINT('',(141.760942367476,255.,-40.1560420081102));
#27671=CARTESIAN_POINT('',(141.760942367476,294.,-40.1560420081102));
#27672=CARTESIAN_POINT('Origin',(142.508521203919,255.,-39.4187321117283));
#27673=CARTESIAN_POINT('',(141.458521203919,280.,-39.4187321117283));
#27674=CARTESIAN_POINT('Origin',(142.508521203919,280.,-39.4187321117283));
#27675=CARTESIAN_POINT('',(141.458521203919,294.,-39.4187321117283));
#27676=CARTESIAN_POINT('',(141.458521203919,255.,-39.4187321117283));
#27677=CARTESIAN_POINT('Origin',(142.508521203919,294.,-39.4187321117283));
#27678=CARTESIAN_POINT('Origin',(141.458521203919,255.,-39.4187321117283));
#27679=CARTESIAN_POINT('',(141.458521203919,280.,-37.9151793916432));
#27680=CARTESIAN_POINT('',(141.45852120392,280.,-19.7093660558643));
#27681=CARTESIAN_POINT('',(141.458521203919,294.,-37.9151793916432));
#27682=CARTESIAN_POINT('',(141.458521203919,255.,-37.9151793916432));
#27683=CARTESIAN_POINT('',(141.458521203919,294.,-37.9151793916432));
#27684=CARTESIAN_POINT('Origin',(142.508521203919,255.,-37.9151793916432));
#27685=CARTESIAN_POINT('',(141.763569006683,280.,-37.1752157277839));
#27686=CARTESIAN_POINT('Origin',(142.508521203919,280.,-37.9151793916432));
#27687=CARTESIAN_POINT('',(141.763569006683,294.,-37.1752157277839));
#27688=CARTESIAN_POINT('',(141.763569006683,255.,-37.1752157277839));
#27689=CARTESIAN_POINT('Origin',(142.508521203919,294.,-37.9151793916432));
#27690=CARTESIAN_POINT('Origin',(141.763569006683,255.,-37.1752157277839));
#27691=CARTESIAN_POINT('',(144.417668112103,280.,-34.5032237681314));
#27692=CARTESIAN_POINT('',(141.792684822546,280.,-37.1459036249592));
#27693=CARTESIAN_POINT('',(144.417668112103,294.,-34.5032237681314));
#27694=CARTESIAN_POINT('',(144.417668112103,255.,-34.5032237681314));
#27695=CARTESIAN_POINT('',(144.544688744748,294.,-34.375346814161));
#27696=CARTESIAN_POINT('Origin',(144.417668112103,255.,-34.5032237681314));
#27697=CARTESIAN_POINT('',(154.875609963127,280.,-34.5032237681314));
#27698=CARTESIAN_POINT('',(124.436326149411,280.,-34.5032237681314));
#27699=CARTESIAN_POINT('',(154.875609963127,294.,-34.5032237681314));
#27700=CARTESIAN_POINT('',(154.875609963127,255.,-34.5032237681314));
#27701=CARTESIAN_POINT('',(134.86603481566,294.,-34.5032237681314));
#27702=CARTESIAN_POINT('Origin',(154.875609963127,255.,-34.5032237681314));
#27703=CARTESIAN_POINT('',(156.375609963127,280.,-36.0032237681314));
#27704=CARTESIAN_POINT('',(133.644647576992,280.,-13.2722613819965));
#27705=CARTESIAN_POINT('',(156.375609963127,294.,-36.0032237681314));
#27706=CARTESIAN_POINT('',(156.375609963127,255.,-36.0032237681314));
#27707=CARTESIAN_POINT('',(154.875609963127,294.,-34.5032237681314));
#27708=CARTESIAN_POINT('Origin',(156.375609963127,255.,-58.0910625167936));
#27709=CARTESIAN_POINT('',(155.375609963127,280.,-59.0910625167936));
#27710=CARTESIAN_POINT('',(156.375609963127,280.,-58.0910625167936));
#27711=CARTESIAN_POINT('',(154.960007558403,280.,-59.5066649215182));
#27712=CARTESIAN_POINT('',(155.375609963127,294.,-59.0910625167936));
#27713=CARTESIAN_POINT('',(155.375609963127,255.,-59.0910625167936));
#27714=CARTESIAN_POINT('',(156.375609963127,294.,-58.0910625167936));
#27715=CARTESIAN_POINT('',(156.375609963127,294.,-58.0910625167936));
#27716=CARTESIAN_POINT('',(156.375609963127,255.,-58.0910625167936));
#27717=CARTESIAN_POINT('Origin',(155.375609963127,255.,-59.0910625167936));
#27718=CARTESIAN_POINT('',(114.356459668193,280.,-59.0910625167936));
#27719=CARTESIAN_POINT('',(150.62266449878,280.,-59.0910625167936));
#27720=CARTESIAN_POINT('',(114.356459668193,294.,-59.0910625167936));
#27721=CARTESIAN_POINT('',(114.356459668193,255.,-59.0910625167936));
#27722=CARTESIAN_POINT('',(155.375609963127,294.,-59.0910625167936));
#27723=CARTESIAN_POINT('Origin',(114.356459668193,255.,-59.0910625167936));
#27724=CARTESIAN_POINT('',(113.356459668193,280.,-58.0910625167936));
#27725=CARTESIAN_POINT('',(120.773904182304,280.,-65.5085070309049));
#27726=CARTESIAN_POINT('',(113.356459668193,294.,-58.0910625167937));
#27727=CARTESIAN_POINT('',(113.356459668193,255.,-58.0910625167937));
#27728=CARTESIAN_POINT('',(113.356459668193,294.,-58.0910625167937));
#27729=CARTESIAN_POINT('Origin',(113.356459668193,255.,-58.0910625167937));
#27730=CARTESIAN_POINT('',(113.356459668193,280.,-36.0032237681315));
#27731=CARTESIAN_POINT('',(113.356459668193,280.,-29.0455312583968));
#27732=CARTESIAN_POINT('',(113.356459668193,294.,-36.0032237681315));
#27733=CARTESIAN_POINT('',(113.356459668193,255.,-36.0032237681315));
#27734=CARTESIAN_POINT('',(113.356459668193,294.,-36.0032237681315));
#27735=CARTESIAN_POINT('Origin',(113.356459668193,255.,-36.0032237681315));
#27736=CARTESIAN_POINT('',(114.856459668193,280.,-34.5032237681315));
#27737=CARTESIAN_POINT('',(120.131896739857,280.,-29.2277866964671));
#27738=CARTESIAN_POINT('',(114.856459668193,294.,-34.5032237681315));
#27739=CARTESIAN_POINT('',(114.856459668193,255.,-34.5032237681315));
#27740=CARTESIAN_POINT('',(114.856459668193,294.,-34.5032237681315));
#27741=CARTESIAN_POINT('Origin',(114.856459668193,255.,-34.5032237681315));
#27742=CARTESIAN_POINT('',(125.314401519217,280.,-34.5032237681315));
#27743=CARTESIAN_POINT('',(109.655721927456,280.,-34.5032237681315));
#27744=CARTESIAN_POINT('',(125.314401519217,294.,-34.5032237681315));
#27745=CARTESIAN_POINT('',(125.314401519217,255.,-34.5032237681315));
#27746=CARTESIAN_POINT('',(134.86603481566,294.,-34.5032237681314));
#27747=CARTESIAN_POINT('Origin',(125.314401519217,255.,-34.5032237681315));
#27748=CARTESIAN_POINT('',(127.968500624638,280.,-37.1752157277839));
#27749=CARTESIAN_POINT('',(111.508973864096,280.,-20.6047255475076));
#27750=CARTESIAN_POINT('',(127.968500624638,294.,-37.1752157277839));
#27751=CARTESIAN_POINT('',(127.968500624638,255.,-37.1752157277839));
#27752=CARTESIAN_POINT('',(127.968500624638,294.,-37.1752157277839));
#27753=CARTESIAN_POINT('Origin',(127.223548427401,255.,-37.9151793916432));
#27754=CARTESIAN_POINT('',(128.273548427401,280.,-37.9151793916432));
#27755=CARTESIAN_POINT('Origin',(127.223548427401,280.,-37.9151793916432));
#27756=CARTESIAN_POINT('',(128.273548427401,294.,-37.9151793916432));
#27757=CARTESIAN_POINT('',(128.273548427401,255.,-37.9151793916432));
#27758=CARTESIAN_POINT('Origin',(127.223548427401,294.,-37.9151793916432));
#27759=CARTESIAN_POINT('Origin',(134.86603481566,294.,-46.7971431424625));
#27760=CARTESIAN_POINT('',(127.971127263844,294.,-40.1560420081102));
#27761=CARTESIAN_POINT('',(128.273548427401,294.,-39.4187321117283));
#27762=CARTESIAN_POINT('Origin',(127.223548427401,294.,-39.4187321117283));
#27763=CARTESIAN_POINT('',(127.333356762198,294.,-40.8026951072716));
#27764=CARTESIAN_POINT('',(127.333356762198,294.,-40.8026951072716));
#27765=CARTESIAN_POINT('',(126.997701127708,294.,-41.3560806824536));
#27766=CARTESIAN_POINT('Origin',(128.330128544122,294.,-41.785774969114));
#27767=CARTESIAN_POINT('',(125.328762843953,294.,-42.9220241352404));
#27768=CARTESIAN_POINT('Origin',(124.747780443448,294.,-40.6305041508116));
#27769=CARTESIAN_POINT('',(124.876218876064,294.,-43.5036225521864));
#27770=CARTESIAN_POINT('Origin',(125.476218876064,294.,-43.5036225521863));
#27771=CARTESIAN_POINT('',(124.876218876064,294.,-44.4226470147914));
#27772=CARTESIAN_POINT('',(124.876218876064,294.,-44.4226470147914));
#27773=CARTESIAN_POINT('',(125.387243744723,294.,-45.1153516005764));
#27774=CARTESIAN_POINT('Origin',(125.601218876064,294.,-44.4226470147914));
#27775=CARTESIAN_POINT('',(127.036092546462,294.,-46.8112703207193));
#27776=CARTESIAN_POINT('Origin',(124.659008759128,294.,-47.4728765656934));
#27777=CARTESIAN_POINT('',(127.149786002621,294.,-47.007169160326));
#27778=CARTESIAN_POINT('Origin',(127.469614165074,294.,-46.690609613792));
#27779=CARTESIAN_POINT('',(127.637659789347,294.,-47.5000804575095));
#27780=CARTESIAN_POINT('',(127.637659789347,294.,-47.5000804575095));
#27781=CARTESIAN_POINT('',(142.094409841973,294.,-47.5000804575095));
#27782=CARTESIAN_POINT('',(142.094409841973,294.,-47.5000804575095));
#27783=CARTESIAN_POINT('',(142.5822836287,294.,-47.007169160326));
#27784=CARTESIAN_POINT('',(142.5822836287,294.,-47.007169160326));
#27785=CARTESIAN_POINT('',(142.695977084858,294.,-46.8112703207193));
#27786=CARTESIAN_POINT('Origin',(142.262455466246,294.,-46.690609613792));
#27787=CARTESIAN_POINT('',(144.344825886597,294.,-45.1153516005764));
#27788=CARTESIAN_POINT('Origin',(145.073060872192,294.,-47.4728765656934));
#27789=CARTESIAN_POINT('',(144.855850755256,294.,-44.4226470147914));
#27790=CARTESIAN_POINT('Origin',(144.130850755256,294.,-44.4226470147914));
#27791=CARTESIAN_POINT('',(144.855850755256,294.,-43.5036225521863));
#27792=CARTESIAN_POINT('',(144.855850755256,294.,-43.5036225521863));
#27793=CARTESIAN_POINT('',(144.403306787367,294.,-42.9220241352404));
#27794=CARTESIAN_POINT('Origin',(144.255850755256,294.,-43.5036225521863));
#27795=CARTESIAN_POINT('Origin',(144.984289187872,294.,-40.6305041508117));
#27796=CARTESIAN_POINT('',(156.375609963127,294.,-36.0032237681314));
#27797=CARTESIAN_POINT('',(128.273548427401,294.,-39.4187321117283));
#27798=CARTESIAN_POINT('Origin',(156.375609963127,255.,-36.0032237681314));
#27799=CARTESIAN_POINT('',(156.375609963127,280.,-18.0016118840657));
#27800=CARTESIAN_POINT('Origin',(128.273548427401,255.,-37.9151793916432));
#27801=CARTESIAN_POINT('',(128.273548427401,280.,-39.4187321117283));
#27802=CARTESIAN_POINT('',(128.273548427401,280.,-18.9575896958216));
#27803=CARTESIAN_POINT('',(128.273548427401,255.,-39.4187321117283));
#27804=CARTESIAN_POINT('Origin',(127.223548427401,255.,-39.4187321117283));
#27805=CARTESIAN_POINT('',(127.971127263844,280.,-40.1560420081102));
#27806=CARTESIAN_POINT('Origin',(127.223548427401,280.,-39.4187321117283));
#27807=CARTESIAN_POINT('',(127.971127263844,255.,-40.1560420081102));
#27808=CARTESIAN_POINT('Origin',(127.971127263844,255.,-40.1560420081102));
#27809=CARTESIAN_POINT('',(127.333356762198,280.,-40.8026951072716));
#27810=CARTESIAN_POINT('',(132.211452368059,280.,-35.85665945119));
#27811=CARTESIAN_POINT('',(127.333356762198,255.,-40.8026951072716));
#27812=CARTESIAN_POINT('Origin',(128.330128544122,255.,-41.785774969114));
#27813=CARTESIAN_POINT('',(126.997701127708,280.,-41.3560806824536));
#27814=CARTESIAN_POINT('Origin',(128.330128544122,280.,-41.785774969114));
#27815=CARTESIAN_POINT('',(126.997701127708,255.,-41.3560806824536));
#27816=CARTESIAN_POINT('Origin',(124.747780443448,255.,-40.6305041508116));
#27817=CARTESIAN_POINT('',(125.328762843953,280.,-42.9220241352404));
#27818=CARTESIAN_POINT('Origin',(124.747780443448,280.,-40.6305041508116));
#27819=CARTESIAN_POINT('',(125.328762843953,255.,-42.9220241352404));
#27820=CARTESIAN_POINT('Origin',(125.476218876064,255.,-43.5036225521863));
#27821=CARTESIAN_POINT('',(124.876218876064,280.,-43.5036225521864));
#27822=CARTESIAN_POINT('Origin',(125.476218876064,280.,-43.5036225521863));
#27823=CARTESIAN_POINT('',(124.876218876064,255.,-43.5036225521864));
#27824=CARTESIAN_POINT('Origin',(124.876218876064,255.,-43.5036225521864));
#27825=CARTESIAN_POINT('',(124.876218876064,280.,-44.4226470147914));
#27826=CARTESIAN_POINT('',(124.876218876064,280.,-21.751811276093));
#27827=CARTESIAN_POINT('',(124.876218876064,255.,-44.4226470147914));
#27828=CARTESIAN_POINT('Origin',(125.601218876064,255.,-44.4226470147914));
#27829=CARTESIAN_POINT('',(125.387243744723,280.,-45.1153516005764));
#27830=CARTESIAN_POINT('Origin',(125.601218876064,280.,-44.4226470147914));
#27831=CARTESIAN_POINT('',(125.387243744723,255.,-45.1153516005764));
#27832=CARTESIAN_POINT('Origin',(124.659008759128,255.,-47.4728765656934));
#27833=CARTESIAN_POINT('',(127.036092546462,280.,-46.8112703207193));
#27834=CARTESIAN_POINT('Origin',(124.659008759128,280.,-47.4728765656934));
#27835=CARTESIAN_POINT('',(127.036092546462,255.,-46.8112703207193));
#27836=CARTESIAN_POINT('Origin',(127.469614165074,255.,-46.690609613792));
#27837=CARTESIAN_POINT('',(127.149786002621,280.,-47.007169160326));
#27838=CARTESIAN_POINT('Origin',(127.469614165074,280.,-46.690609613792));
#27839=CARTESIAN_POINT('',(127.149786002621,255.,-47.007169160326));
#27840=CARTESIAN_POINT('Origin',(127.149786002621,255.,-47.007169160326));
#27841=CARTESIAN_POINT('',(127.637659789347,280.,-47.5000804575095));
#27842=CARTESIAN_POINT('',(109.783194287684,280.,-29.4612597821981));
#27843=CARTESIAN_POINT('',(127.637659789347,255.,-47.5000804575095));
#27844=CARTESIAN_POINT('Origin',(127.637659789347,255.,-47.5000804575095));
#27845=CARTESIAN_POINT('',(142.094409841973,280.,-47.5000804575095));
#27846=CARTESIAN_POINT('',(116.046321988033,280.,-47.5000804575095));
#27847=CARTESIAN_POINT('',(142.094409841973,255.,-47.5000804575095));
#27848=CARTESIAN_POINT('Origin',(142.094409841973,255.,-47.5000804575095));
#27849=CARTESIAN_POINT('',(142.5822836287,280.,-47.007169160326));
#27850=CARTESIAN_POINT('',(144.655606318974,280.,-44.9124385054979));
#27851=CARTESIAN_POINT('',(142.5822836287,255.,-47.007169160326));
#27852=CARTESIAN_POINT('Origin',(142.262455466246,255.,-46.690609613792));
#27853=CARTESIAN_POINT('',(142.695977084858,280.,-46.8112703207193));
#27854=CARTESIAN_POINT('Origin',(142.262455466246,280.,-46.690609613792));
#27855=CARTESIAN_POINT('',(142.695977084858,255.,-46.8112703207193));
#27856=CARTESIAN_POINT('Origin',(145.073060872192,255.,-47.4728765656934));
#27857=CARTESIAN_POINT('',(144.344825886597,280.,-45.1153516005764));
#27858=CARTESIAN_POINT('Origin',(145.073060872192,280.,-47.4728765656934));
#27859=CARTESIAN_POINT('',(144.344825886597,255.,-45.1153516005764));
#27860=CARTESIAN_POINT('Origin',(144.130850755256,255.,-44.4226470147914));
#27861=CARTESIAN_POINT('',(144.855850755256,280.,-44.4226470147914));
#27862=CARTESIAN_POINT('Origin',(144.130850755256,280.,-44.4226470147914));
#27863=CARTESIAN_POINT('',(144.855850755256,255.,-44.4226470147914));
#27864=CARTESIAN_POINT('Origin',(144.855850755256,255.,-44.4226470147914));
#27865=CARTESIAN_POINT('',(144.855850755256,280.,-43.5036225521863));
#27866=CARTESIAN_POINT('',(144.855850755256,280.,-22.2113235073957));
#27867=CARTESIAN_POINT('',(144.855850755256,255.,-43.5036225521863));
#27868=CARTESIAN_POINT('Origin',(144.255850755256,255.,-43.5036225521863));
#27869=CARTESIAN_POINT('',(144.403306787367,280.,-42.9220241352404));
#27870=CARTESIAN_POINT('Origin',(144.255850755256,280.,-43.5036225521863));
#27871=CARTESIAN_POINT('',(144.403306787367,255.,-42.9220241352404));
#27872=CARTESIAN_POINT('Origin',(144.984289187872,255.,-40.6305041508117));
#27873=CARTESIAN_POINT('Origin',(144.984289187872,280.,-40.6305041508117));
#27874=CARTESIAN_POINT('Origin',(104.454984186719,280.,0.));
#48345=UNCERTAINTY_MEASURE_WITH_UNIT(LENGTH_MEASURE(0.01),#48370,
'DISTANCE_ACCURACY_VALUE',
'Maximum model space distance between geometric entities at asserted c
onnectivities');
#48356=UNCERTAINTY_MEASURE_WITH_UNIT(LENGTH_MEASURE(0.01),#48370,
'DISTANCE_ACCURACY_VALUE',
'Maximum model space distance between geometric entities at asserted c
onnectivities');
#48358=(
GEOMETRIC_REPRESENTATION_CONTEXT(3)
GLOBAL_UNCERTAINTY_ASSIGNED_CONTEXT((#48345))
GLOBAL_UNIT_ASSIGNED_CONTEXT((#48370,#48372,#48373))
REPRESENTATION_CONTEXT('','3D')
);
#48369=(
GEOMETRIC_REPRESENTATION_CONTEXT(3)
GLOBAL_UNCERTAINTY_ASSIGNED_CONTEXT((#48356))
GLOBAL_UNIT_ASSIGNED_CONTEXT((#48370,#48372,#48373))
REPRESENTATION_CONTEXT('','3D')
);
#48370=(
LENGTH_UNIT()
NAMED_UNIT(*)
SI_UNIT(.MILLI.,.METRE.)
);
#48372=(
NAMED_UNIT(*)
PLANE_ANGLE_UNIT()
SI_UNIT($,.RADIAN.)
);
#48373=(
NAMED_UNIT(*)
SI_UNIT($,.STERADIAN.)
SOLID_ANGLE_UNIT()
);
#48375=SHAPE_DEFINITION_REPRESENTATION(#48387,#48413);
#48387=PRODUCT_DEFINITION_SHAPE('',$,#48426);
#48413=SHAPE_REPRESENTATION('',(#20257),#48358);
#48424=PRODUCT_DEFINITION_CONTEXT('part definition',#48462,'design');
#48426=PRODUCT_DEFINITION('LINEAR GUIDE(Mirror)','LINEAR GUIDE(Mirror)',
#48438,#48424);
#48438=PRODUCT_DEFINITION_FORMATION('',$,#48465);
#48462=APPLICATION_CONTEXT(
'Core Data for Automotive Mechanical Design Process');
#48463=PRODUCT_CONTEXT('part definition',#48462,'mechanical');
#48465=PRODUCT('LINEAR GUIDE(Mirror)','LINEAR GUIDE(Mirror)',$,(#48463));
#48504=COLOUR_RGB('Sky Blue',0.24,0.69,0.87);
#48505=FILL_AREA_STYLE_COLOUR('',#48504);
#48506=FILL_AREA_STYLE('',(#48505));
#48507=SURFACE_STYLE_FILL_AREA(#48506);
#48508=SURFACE_SIDE_STYLE('',(#48507));
#48509=SURFACE_STYLE_USAGE(.BOTH.,#48508);
#48510=PRESENTATION_STYLE_ASSIGNMENT((#48509));
ENDSEC;
END-ISO-10303-21;
